ISO-10303-21;
HEADER;
FILE_DESCRIPTION (('STEP AP214'),
    '1' );
FILE_NAME ('Part 130_Varsay\X2\0131\X0\lan.step',
    '2026-10-08T11:03:28',
    ( '' ),
    ( '' ),
    'SwSTEP 2.0',
    'SolidWorks 2024',
    '' );
FILE_SCHEMA (( 'AUTOMOTIVE_DESIGN' ));
ENDSEC;

DATA;
#7=VECTOR ( 'NONE', #913, 1000.000000000000000 ) ;
#8=LINE ( 'NONE', #2469, #3092 ) ;
#9=VECTOR ( 'NONE', #126, 1000.000000000000000 ) ;
#12=PLANE ( 'NONE',  #3351 ) ;
#13=EDGE_CURVE ( 'NONE', #1212, #3737, #2435, .T. ) ;
#15=CYLINDRICAL_SURFACE ( 'NONE', #4136, 0.7500000000000006661 ) ;
#16=CYLINDRICAL_SURFACE ( 'NONE', #1372, 0.7499999999999997780 ) ;
#17=FILL_AREA_STYLE_COLOUR ( '', #4215 ) ;
#18=AXIS2_PLACEMENT_3D ( 'NONE', #23, #1540, #3973 ) ;
#19=CARTESIAN_POINT ( 'NONE',  ( 11.96600549393350299, -7.807631214078937454, 17.65096039353564805 ) ) ;
#22=DIRECTION ( 'NONE',  ( 1.000000000000000000, 1.076498916035107621E-16, -0.000000000000000000 ) ) ;
#23=CARTESIAN_POINT ( 'NONE',  ( -6.869994990996021400, -6.397499167952784838, 18.40096039353565160 ) ) ;
#26=EDGE_LOOP ( 'NONE', ( #2589, #425, #54, #3081 ) ) ;
#28=AXIS2_PLACEMENT_3D ( 'NONE', #4115, #895, #1519 ) ;
#36=EDGE_CURVE ( 'NONE', #2260, #2464, #1685, .T. ) ;
#38=DIRECTION ( 'NONE',  ( -0.000000000000000000, -0.000000000000000000, -1.000000000000000000 ) ) ;
#40=DIRECTION ( 'NONE',  ( 0.000000000000000000, 1.000000000000000000, 0.000000000000000000 ) ) ;
#42=( NAMED_UNIT ( * ) SI_UNIT ( $, .STERADIAN. ) SOLID_ANGLE_UNIT ( ) );
#45=CARTESIAN_POINT ( 'NONE',  ( 14.28750500900398279, 8.320472145597748469E-07, 17.65096039353565160 ) ) ;
#49=VECTOR ( 'NONE', #2598, 1000.000000000000000 ) ;
#50=ORIENTED_EDGE ( 'NONE', *, *, #62, .T. ) ;
#53=ORIENTED_EDGE ( 'NONE', *, *, #4114, .T. ) ;
#54=ORIENTED_EDGE ( 'NONE', *, *, #659, .F. ) ;
#60=CARTESIAN_POINT ( 'NONE',  ( -14.12140203323284204, 2.180955620240156545, 29.52533606476202621 ) ) ;
#62=EDGE_CURVE ( 'NONE', #3737, #4361, #8, .T. ) ;
#67=CARTESIAN_POINT ( 'NONE',  ( -17.48249499099600968, -7.897499167952782173, 18.40096039353565160 ) ) ;
#68=FACE_OUTER_BOUND ( 'NONE', #2702, .T. ) ;
#70=CARTESIAN_POINT ( 'NONE',  ( -8.369994990996016071, 6.397500832047212427, 17.65096039353565160 ) ) ;
#72=EDGE_CURVE ( 'NONE', #4385, #2774, #2483, .T. ) ;
#73=ORIENTED_EDGE ( 'NONE', *, *, #84, .T. ) ;
#80=CARTESIAN_POINT ( 'NONE',  ( 13.92256467935009034, -3.209909955418536409, 30.77756777369077312 ) ) ;
#83=MECHANICAL_DESIGN_GEOMETRIC_PRESENTATION_REPRESENTATION('',(#914),#4064);
#84=EDGE_CURVE ( 'NONE', #2363, #3745, #1077, .T. ) ;
#87=AXIS2_PLACEMENT_3D ( 'NONE', #761, #3633, #4319 ) ;
#93=CYLINDRICAL_SURFACE ( 'NONE', #677, 3.573749999999999538 ) ;
#104=DIRECTION ( 'NONE',  ( 0.000000000000000000, 1.000000000000000000, -0.000000000000000000 ) ) ;
#108=LINE ( 'NONE', #835, #4367 ) ;
#113=EDGE_CURVE ( 'NONE', #3745, #2828, #2285, .T. ) ;
#115=CARTESIAN_POINT ( 'NONE',  ( 6.870005009003977037, -6.397499167952786614, 18.40096039353565160 ) ) ;
#119=AXIS2_PLACEMENT_3D ( 'NONE', #3333, #3405, #2246 ) ;
#120=EDGE_CURVE ( 'NONE', #4361, #2188, #836, .T. ) ;
#122=EDGE_LOOP ( 'NONE', ( #2207, #3885, #1345, #218 ) ) ;
#123=EDGE_CURVE ( 'NONE', #2304, #1592, #1177, .T. ) ;
#124=ORIENTED_EDGE ( 'NONE', *, *, #4476, .F. ) ;
#126=DIRECTION ( 'NONE',  ( -0.000000000000000000, -0.000000000000000000, -1.000000000000000000 ) ) ;
#127=ORIENTED_EDGE ( 'NONE', *, *, #123, .T. ) ;
#129=DIRECTION ( 'NONE',  ( 0.000000000000000000, 0.000000000000000000, 1.000000000000000000 ) ) ;
#156=CARTESIAN_POINT ( 'NONE',  ( -12.27094704565411121, 7.318711406274640119, 17.91402383463540104 ) ) ;
#160=CYLINDRICAL_SURFACE ( 'NONE', #3367, 3.573749999999999538 ) ;
#161=ADVANCED_BREP_SHAPE_REPRESENTATION ( '', ( #1920, #4483 ), #2891 ) ;
#162=CIRCLE ( 'NONE', #2984, 0.7500000000000006661 ) ;
#166=EDGE_CURVE ( 'NONE', #1497, #1208, #805, .T. ) ;
#168=DIRECTION ( 'NONE',  ( 0.000000000000000000, -1.000000000000000000, 0.000000000000000000 ) ) ;
#169=CARTESIAN_POINT ( 'NONE',  ( -14.28749499099602005, 0.2372044551111577027, 35.93971039353565544 ) ) ;
#174=CARTESIAN_POINT ( 'NONE',  ( 13.92220474334306601, 3.211459441160700923, 30.78080196879686170 ) ) ;
#184=ORIENTED_EDGE ( 'NONE', *, *, #3116, .F. ) ;
#191=CARTESIAN_POINT ( 'NONE',  ( -13.86254577222764262, 3.458987924946582915, 33.29469953564710494 ) ) ;
#192=CARTESIAN_POINT ( 'NONE',  ( 12.37117714425454551, -7.147499167952784838, 18.40096039353565160 ) ) ;
#195=VERTEX_POINT ( 'NONE', #1570 ) ;
#197=CARTESIAN_POINT ( 'NONE',  ( -7.619994990996017847, 12.08587093932537826, 18.40096039353565160 ) ) ;
#204=CARTESIAN_POINT ( 'NONE',  ( 12.58215065716882819, 6.772263696356577434, 34.69848916189055643 ) ) ;
#206=PLANE ( 'NONE',  #651 ) ;
#209=VERTEX_POINT ( 'NONE', #2989 ) ;
#212=LINE ( 'NONE', #3385, #3482 ) ;
#213=AXIS2_PLACEMENT_3D ( 'NONE', #1164, #1885, #2858 ) ;
#218=ORIENTED_EDGE ( 'NONE', *, *, #2621, .T. ) ;
#224=CARTESIAN_POINT ( 'NONE',  ( -13.60391200005281753, -4.370503985835838101, 38.02622764783903619 ) ) ;
#228=ORIENTED_EDGE ( 'NONE', *, *, #1349, .T. ) ;
#230=VERTEX_POINT ( 'NONE', #2325 ) ;
#233=EDGE_CURVE ( 'NONE', #4049, #680, #4434, .T. ) ;
#234=B_SPLINE_CURVE_WITH_KNOTS ( 'NONE', 3,
 ( #3727, #507, #4132, #3380, #204, #4464, #1951, #2335, #1251, #1299, #2666, #4107, #885, #2310, #3778, #1654, #3071, #4513, #2716, #4157, #2353, #3798, #2021, #3520 ),
 .UNSPECIFIED., .F., .F.,
 ( 4, 2, 2, 2, 2, 2, 2, 2, 2, 2, 2, 4 ),
 ( 0.000000000000000000, 0.001420218485702516619, 0.002840436971405033238, 0.004260655457107550073, 0.004970764699958816514, 0.005680873942810082955, 0.006390983185661350263, 0.007101092428512616704, 0.008521310914215162596, 0.009231420157066438578, 0.009941529399917716295, 0.01136174788562026999 ),
 .UNSPECIFIED. ) ;
#239=DIRECTION ( 'NONE',  ( 1.000000000000000000, 1.076498916035107621E-16, -0.000000000000000000 ) ) ;
#246=FACE_OUTER_BOUND ( 'NONE', #1430, .T. ) ;
#247=CARTESIAN_POINT ( 'NONE',  ( 14.28750500900398279, 8.320472145953950175E-07, 35.93971039353566965 ) ) ;
#248=CARTESIAN_POINT ( 'NONE',  ( -13.92229192741629262, -3.211036282058272739, 33.95194610545058822 ) ) ;
#250=FACE_OUTER_BOUND ( 'NONE', #4509, .T. ) ;
#258=LINE ( 'NONE', #3153, #4263 ) ;
#262=ORIENTED_EDGE ( 'NONE', *, *, #4295, .T. ) ;
#265=EDGE_CURVE ( 'NONE', #2363, #680, #2439, .T. ) ;
#269=CARTESIAN_POINT ( 'NONE',  ( -14.17582296520950713, -1.793657354674257354, 35.46585984560420712 ) ) ;
#270=CARTESIAN_POINT ( 'NONE',  ( 13.83079035606262508, -3.606001054908336112, 38.55461960823348022 ) ) ;
#272=CARTESIAN_POINT ( 'NONE',  ( -14.28749499099602005, 8.320472128100571937E-07, 28.79221039353566880 ) ) ;
#276=DIRECTION ( 'NONE',  ( -1.000000000000000000, 1.076498916035107744E-16, 0.000000000000000000 ) ) ;
#280=EDGE_CURVE ( 'NONE', #719, #1143, #3487, .T. ) ;
#287=ORIENTED_EDGE ( 'NONE', *, *, #1174, .F. ) ;
#288=DIRECTION ( 'NONE',  ( 0.000000000000000000, 0.000000000000000000, 1.000000000000000000 ) ) ;
#293=CARTESIAN_POINT ( 'NONE',  ( 12.58716054243624249, -6.760358215630333234, 34.69836126359587070 ) ) ;
#296=DIRECTION ( 'NONE',  ( 0.000000000000000000, -0.000000000000000000, -1.000000000000000000 ) ) ;
#301=VECTOR ( 'NONE', #694, 1000.000000000000000 ) ;
#304=LINE ( 'NONE', #2457, #806 ) ;
#310=ORIENTED_EDGE ( 'NONE', *, *, #1590, .T. ) ;
#314=DIRECTION ( 'NONE',  ( 1.000000000000000000, 0.000000000000000000, 0.000000000000000000 ) ) ;
#315=ORIENTED_EDGE ( 'NONE', *, *, #4091, .F. ) ;
#318=CARTESIAN_POINT ( 'NONE',  ( -14.05880083816784598, -2.555479569424798036, 39.04506677964694461 ) ) ;
#321=DIRECTION ( 'NONE',  ( 0.000000000000000000, 0.000000000000000000, 1.000000000000000000 ) ) ;
#322=CARTESIAN_POINT ( 'NONE',  ( -13.92260781862683672, -3.209692932854570024, 30.77693904423523819 ) ) ;
#325=DIRECTION ( 'NONE',  ( 0.000000000000000000, 0.000000000000000000, 1.000000000000000000 ) ) ;
#331=DIRECTION ( 'NONE',  ( 0.000000000000000000, -1.000000000000000000, 0.000000000000000000 ) ) ;
#335=EDGE_LOOP ( 'NONE', ( #948, #1406 ) ) ;
#337=CARTESIAN_POINT ( 'NONE',  ( 12.35764254201991719, 7.171053272434127379, 18.18681329310062011 ) ) ;
#341=DIRECTION ( 'NONE',  ( 0.000000000000000000, -0.000000000000000000, 1.000000000000000000 ) ) ;
#349=CARTESIAN_POINT ( 'NONE',  ( 3.750005009003979595, 3.750000832047212906, 18.79096039353565217 ) ) ;
#351=CARTESIAN_POINT ( 'NONE',  ( 13.83333314027810701, 3.573750832047211112, 32.83350159718256123 ) ) ;
#352=AXIS2_PLACEMENT_3D ( 'NONE', #3185, #4020, #314 ) ;
#360=CARTESIAN_POINT ( 'NONE',  ( 12.27079714706309055, 7.318983740777395219, 17.91363472736960816 ) ) ;
#373=ORIENTED_EDGE ( 'NONE', *, *, #3936, .F. ) ;
#375=EDGE_CURVE ( 'NONE', #2669, #3403, #4284, .T. ) ;
#379=ORIENTED_EDGE ( 'NONE', *, *, #3374, .F. ) ;
#393=FILL_AREA_STYLE ('',( #17 ) ) ;
#396=ORIENTED_EDGE ( 'NONE', *, *, #2346, .T. ) ;
#397=CARTESIAN_POINT ( 'NONE',  ( 14.00306134798043800, 2.839839263610262954, 34.54803640670024123 ) ) ;
#409=CARTESIAN_POINT ( 'NONE',  ( -8.369994990996016071, 6.397500832047212427, 18.40096039353565160 ) ) ;
#410=PLANE ( 'NONE',  #1786 ) ;
#411=CARTESIAN_POINT ( 'NONE',  ( -13.87970419316790682, -3.390420155928260293, 31.21176438016646770 ) ) ;
#415=CARTESIAN_POINT ( 'NONE',  ( 12.30738649273683372, -7.256959721446875733, 17.99723211794410460 ) ) ;
#417=ORIENTED_EDGE ( 'NONE', *, *, #13, .T. ) ;
#418=DIRECTION ( 'NONE',  ( -1.000000000000000000, -1.076498916035107621E-16, 0.000000000000000000 ) ) ;
#420=DIRECTION ( 'NONE',  ( 1.000000000000000000, 0.000000000000000000, 0.000000000000000000 ) ) ;
#422=CIRCLE ( 'NONE', #2440, 0.7500000000000006661 ) ;
#425=ORIENTED_EDGE ( 'NONE', *, *, #601, .F. ) ;
#427=DIRECTION ( 'NONE',  ( 1.000000000000000000, -0.000000000000000000, -0.000000000000000000 ) ) ;
#428=CARTESIAN_POINT ( 'NONE',  ( 14.28155663460688984, 0.4719428512367060402, 28.81578682141157444 ) ) ;
#429=EDGE_CURVE ( 'NONE', #4385, #3952, #3669, .T. ) ;
#434=CARTESIAN_POINT ( 'NONE',  ( 14.99250500900398109, 7.147500832047209762, 32.36596039353565857 ) ) ;
#436=CIRCLE ( 'NONE', #2760, 0.7500000000000006661 ) ;
#439=DIRECTION ( 'NONE',  ( 0.000000000000000000, 0.000000000000000000, 1.000000000000000000 ) ) ;
#450=CARTESIAN_POINT ( 'NONE',  ( -13.48424419627515292, 4.726824056057109757, 37.73224719609674338 ) ) ;
#452=CARTESIAN_POINT ( 'NONE',  ( -13.23918051912923666, 5.374175169457920731, 37.08379739163955691 ) ) ;
#463=CARTESIAN_POINT ( 'NONE',  ( -7.619994990996021400, -6.397499167952786614, 32.36596039353565857 ) ) ;
#466=CARTESIAN_POINT ( 'NONE',  ( 3.750005009003979595, -3.749999167952787538, 18.79096039353565217 ) ) ;
#484=DIRECTION ( 'NONE',  ( -1.076498916035107621E-16, -1.000000000000000000, 0.000000000000000000 ) ) ;
#486=ORIENTED_EDGE ( 'NONE', *, *, #120, .F. ) ;
#487=CARTESIAN_POINT ( 'NONE',  ( -12.37116712624658810, -7.147499167952783061, 17.65096039353565160 ) ) ;
#495=ORIENTED_EDGE ( 'NONE', *, *, #520, .F. ) ;
#497=CARTESIAN_POINT ( 'NONE',  ( 13.86272949647482200, 3.458292335070031864, 31.43485104414858711 ) ) ;
#500=PRODUCT_DEFINITION ( 'UNKNOWN', '', #3721, #1613 ) ;
#504=( NAMED_UNIT ( * ) PLANE_ANGLE_UNIT ( ) SI_UNIT ( $, .RADIAN. ) );
#506=DIRECTION ( 'NONE',  ( -1.000000000000000000, 1.076498916035107744E-16, 0.000000000000000000 ) ) ;
#507=CARTESIAN_POINT ( 'NONE',  ( 12.37117714425454551, 7.147500832047209762, 32.84697568125973532 ) ) ;
#511=ORIENTED_EDGE ( 'NONE', *, *, #2401, .F. ) ;
#512=CARTESIAN_POINT ( 'NONE',  ( 6.870005009003979701, 8.320472135496153183E-07, 17.65096039353565160 ) ) ;
#514=TOROIDAL_SURFACE ( 'NONE', #1725, 6.397499999999999964, 0.7500000000000000000 ) ;
#515=ORIENTED_EDGE ( 'NONE', *, *, #3366, .F. ) ;
#517=CARTESIAN_POINT ( 'NONE',  ( -14.00302961127090029, 2.839984366820609729, 34.54801793703359891 ) ) ;
#520=EDGE_CURVE ( 'NONE', #2793, #952, #4405, .T. ) ;
#521=CARTESIAN_POINT ( 'NONE',  ( 13.83333314027810701, 3.573750832047210668, 32.36596039353566567 ) ) ;
#525=CARTESIAN_POINT ( 'NONE',  ( 3.750005009003979595, -3.749999167952787538, 3.790960393535649064 ) ) ;
#527=EDGE_CURVE ( 'NONE', #2126, #1592, #1914, .T. ) ;
#544=CARTESIAN_POINT ( 'NONE',  ( -13.92217922470506153, 3.211518876436516567, 33.95088485475975659 ) ) ;
#545=CARTESIAN_POINT ( 'NONE',  ( -7.619994990996011630, 7.897500832047212427, 17.65096039353565160 ) ) ;
#550=CARTESIAN_POINT ( 'NONE',  ( 13.83333314027810701, 3.573750832047211112, 32.13223144433574419 ) ) ;
#551=ORIENTED_EDGE ( 'NONE', *, *, #1276, .F. ) ;
#554=DIRECTION ( 'NONE',  ( 0.000000000000000000, 0.000000000000000000, 1.000000000000000000 ) ) ;
#561=CARTESIAN_POINT ( 'NONE',  ( 7.620005009003980589, -6.397499167952787502, 32.36596039353565857 ) ) ;
#563=VERTEX_POINT ( 'NONE', #4475 ) ;
#565=CARTESIAN_POINT ( 'NONE',  ( -3.749994990996019517, 3.750000832047212906, 17.65096039353565160 ) ) ;
#569=UNCERTAINTY_MEASURE_WITH_UNIT (LENGTH_MEASURE( 1.000000000000000082E-05 ), #2969, 'distance_accuracy_value', 'NONE');
#570=EDGE_LOOP ( 'NONE', ( #1120, #2843, #4288, #3872 ) ) ;
#572=AXIS2_PLACEMENT_3D ( 'NONE', #953, #4576, #2038 ) ;
#575=CARTESIAN_POINT ( 'NONE',  ( -13.83934635305755378, -3.550665210907423930, 32.83413998674555501 ) ) ;
#579=VECTOR ( 'NONE', #1317, 1000.000000000000000 ) ;
#581=ORIENTED_EDGE ( 'NONE', *, *, #1923, .F. ) ;
#583=CARTESIAN_POINT ( 'NONE',  ( -11.90638613189174144, -7.897499167952782173, 17.65096039353565160 ) ) ;
#584=ORIENTED_EDGE ( 'NONE', *, *, #4023, .T. ) ;
#592=VECTOR ( 'NONE', #3864, 1000.000000000000000 ) ;
#597=CARTESIAN_POINT ( 'NONE',  ( -12.58214063916086722, -6.772262032262147180, 34.69848916189056354 ) ) ;
#598=CARTESIAN_POINT ( 'NONE',  ( 13.60368842669744538, -4.371226900785080360, 38.02566532807936994 ) ) ;
#599=DIRECTION ( 'NONE',  ( 9.517981353260378315E-33, 8.841607930564763213E-17, -1.000000000000000000 ) ) ;
#600=EDGE_CURVE ( 'NONE', #2299, #1212, #1035, .T. ) ;
#601=EDGE_CURVE ( 'NONE', #1592, #1729, #2328, .T. ) ;
#602=CARTESIAN_POINT ( 'NONE',  ( -14.20090908106113403, -1.585388553952144175, 29.15464480295243277 ) ) ;
#616=CIRCLE ( 'NONE', #1458, 14.28750000000000142 ) ;
#617=CARTESIAN_POINT ( 'NONE',  ( 3.750005009003979595, -3.749999167952787538, 18.79096039353565217 ) ) ;
#622=CARTESIAN_POINT ( 'NONE',  ( -12.37116712624658810, -7.147499167952783061, 32.36596039353565857 ) ) ;
#623=CARTESIAN_POINT ( 'NONE',  ( 12.47854901097075597, -6.958554981044172472, 34.01560235227155715 ) ) ;
#625=CARTESIAN_POINT ( 'NONE',  ( 14.28750500900398279, 8.320472145953950175E-07, 35.93971039353566965 ) ) ;
#628=CARTESIAN_POINT ( 'NONE',  ( -7.619994990996021400, -7.147499167952783061, 18.40096039353565160 ) ) ;
#629=DIRECTION ( 'NONE',  ( -1.000000000000000000, 0.000000000000000000, 0.000000000000000000 ) ) ;
#631=CARTESIAN_POINT ( 'NONE',  ( -17.48249499099600968, -7.147499167952783061, 32.36596039353565857 ) ) ;
#640=CARTESIAN_POINT ( 'NONE',  ( -13.48443333977609626, -4.726286587311965270, 37.73272338279510763 ) ) ;
#642=CARTESIAN_POINT ( 'NONE',  ( -7.619994990996021400, -6.397499167952784838, 17.65096039353565160 ) ) ;
#643=EDGE_CURVE ( 'NONE', #2188, #2506, #1347, .T. ) ;
#645=VECTOR ( 'NONE', #1619, 1000.000000000000000 ) ;
#651=AXIS2_PLACEMENT_3D ( 'NONE', #3780, #4442, #484 ) ;
#652=CARTESIAN_POINT ( 'NONE',  ( -8.369994990996019624, 8.320472137110901854E-07, 32.36596039353565857 ) ) ;
#655=FACE_OUTER_BOUND ( 'NONE', #122, .T. ) ;
#656=FACE_OUTER_BOUND ( 'NONE', #2707, .T. ) ;
#659=EDGE_CURVE ( 'NONE', #2566, #1592, #1893, .T. ) ;
#662=ORIENTED_EDGE ( 'NONE', *, *, #4578, .T. ) ;
#664=ORIENTED_EDGE ( 'NONE', *, *, #3366, .T. ) ;
#668=CARTESIAN_POINT ( 'NONE',  ( -12.39925909105915736, -7.099459522532631794, 33.31797499930306827 ) ) ;
#669=TOROIDAL_SURFACE ( 'NONE', #3076, 1.500000000000000000, 0.7500000000000000000 ) ;
#672=CARTESIAN_POINT ( 'NONE',  ( -14.28749499099602360, 0.2337324564415137751, 28.79221039353567591 ) ) ;
#677=AXIS2_PLACEMENT_3D ( 'NONE', #2160, #3273, #1114 ) ;
#680=VERTEX_POINT ( 'NONE', #2071 ) ;
#689=CARTESIAN_POINT ( 'NONE',  ( 13.87988099929733110, -3.389724456514533912, 31.20998424916602332 ) ) ;
#691=CARTESIAN_POINT ( 'NONE',  ( -13.83947854995182247, -3.550150644751030260, 31.89422947656246521 ) ) ;
#693=DIRECTION ( 'NONE',  ( -0.000000000000000000, 0.000000000000000000, -1.000000000000000000 ) ) ;
#694=DIRECTION ( 'NONE',  ( 1.000000000000000000, -1.076498916035107621E-16, 0.000000000000000000 ) ) ;
#695=DIRECTION ( 'NONE',  ( -1.000000000000000000, 1.076498916035107621E-16, -0.000000000000000000 ) ) ;
#704=CARTESIAN_POINT ( 'NONE',  ( 12.37117714425454551, 7.147500832047207098, 17.65096039353565160 ) ) ;
#708=DIRECTION ( 'NONE',  ( 1.076498916035107744E-16, 1.000000000000000000, 0.000000000000000000 ) ) ;
#710=CARTESIAN_POINT ( 'NONE',  ( 14.24236565909520280, -1.155183429066308998, 28.97606331622595732 ) ) ;
#713=CARTESIAN_POINT ( 'NONE',  ( -14.25898160115544933, 0.9311474368774493859, 28.90767711873708734 ) ) ;
#719=VERTEX_POINT ( 'NONE', #2408 ) ;
#720=CARTESIAN_POINT ( 'NONE',  ( 14.28155188315728807, 0.4717409201294489041, 35.91611237606498719 ) ) ;
#721=CYLINDRICAL_SURFACE ( 'NONE', #3310, 0.7499999999999997780 ) ;
#723=ORIENTED_EDGE ( 'NONE', *, *, #4476, .T. ) ;
#724=VERTEX_POINT ( 'NONE', #3197 ) ;
#731=CARTESIAN_POINT ( 'NONE',  ( 14.28750500900398279, 8.320472145597748469E-07, 28.79221039353566880 ) ) ;
#736=CARTESIAN_POINT ( 'NONE',  ( -13.83332312227014427, 3.573750832047214221, 32.13187428197717566 ) ) ;
#740=( LENGTH_UNIT ( ) NAMED_UNIT ( * ) SI_UNIT ( .MILLI., .METRE. ) );
#743=EDGE_CURVE ( 'NONE', #3745, #4049, #1749, .T. ) ;
#746=DIRECTION ( 'NONE',  ( 0.000000000000000000, -1.000000000000000000, 0.000000000000000000 ) ) ;
#747=EDGE_CURVE ( 'NONE', #1143, #3946, #4587, .T. ) ;
#748=EDGE_CURVE ( 'NONE', #2770, #4203, #1083, .T. ) ;
#752=ORIENTED_EDGE ( 'NONE', *, *, #1769, .F. ) ;
#753=VECTOR ( 'NONE', #4301, 1000.000000000000000 ) ;
#760=CARTESIAN_POINT ( 'NONE',  ( 14.99250500900398109, 7.147500832047209762, 3.790960393535649064 ) ) ;
#761=CARTESIAN_POINT ( 'NONE',  ( -8.369994990996016071, 7.897500832047212427, 18.40096039353565160 ) ) ;
#767=LINE ( 'NONE', #1864, #3140 ) ;
#774=ORIENTED_EDGE ( 'NONE', *, *, #2076, .F. ) ;
#776=ORIENTED_EDGE ( 'NONE', *, *, #429, .F. ) ;
#779=CARTESIAN_POINT ( 'NONE',  ( 14.25899708262535803, 0.9309096077285254900, 28.90765582148817714 ) ) ;
#781=LINE ( 'NONE', #4057, #1971 ) ;
#789=CARTESIAN_POINT ( 'NONE',  ( 14.09171514697193039, 2.363129204819476303, 35.05698690432073761 ) ) ;
#795=FACE_OUTER_BOUND ( 'NONE', #3698, .T. ) ;
#796=CIRCLE ( 'NONE', #4183, 0.7500000000000006661 ) ;
#799=TOROIDAL_SURFACE ( 'NONE', #4032, 6.397499999999999964, 0.7500000000000000000 ) ;
#803=CARTESIAN_POINT ( 'NONE',  ( -14.09151346090570378, 2.364225744170925569, 35.05594847197529873 ) ) ;
#805=LINE ( 'NONE', #3748, #9 ) ;
#806=VECTOR ( 'NONE', #1352, 1000.000000000000000 ) ;
#807=ORIENTED_EDGE ( 'NONE', *, *, #3353, .T. ) ;
#808=ADVANCED_FACE ( 'NONE', ( #2224 ), #16, .F. ) ;
#811=LINE ( 'NONE', #3777, #899 ) ;
#818=AXIS2_PLACEMENT_3D ( 'NONE', #3591, #1859, #4322 ) ;
#820=DIRECTION ( 'NONE',  ( 1.000000000000000000, -1.076498916035107621E-16, 0.000000000000000000 ) ) ;
#823=ORIENTED_EDGE ( 'NONE', *, *, #3835, .T. ) ;
#825=DIRECTION ( 'NONE',  ( 1.076498916035107621E-16, 1.000000000000000000, -0.000000000000000000 ) ) ;
#835=CARTESIAN_POINT ( 'NONE',  ( -3.749994990996019961, -3.749999167952787094, 18.79096039353565217 ) ) ;
#836=CIRCLE ( 'NONE', #1069, 0.7500000000000006661 ) ;
#838=DIRECTION ( 'NONE',  ( 0.000000000000000000, 0.000000000000000000, -1.000000000000000000 ) ) ;
#839=VECTOR ( 'NONE', #2316, 1000.000000000000000 ) ;
#841=CARTESIAN_POINT ( 'NONE',  ( -8.369994990996019624, -6.397499167952784838, 18.40096039353565160 ) ) ;
#842=ORIENTED_EDGE ( 'NONE', *, *, #3937, .T. ) ;
#855=CARTESIAN_POINT ( 'NONE',  ( 8.370005009003978813, -7.897499167952783949, 18.40096039353565160 ) ) ;
#857=CARTESIAN_POINT ( 'NONE',  ( -12.47853899296279501, 6.958556645138596508, 34.01560235227155715 ) ) ;
#862=CARTESIAN_POINT ( 'NONE',  ( 18.74250500900397753, 3.573750832047210224, 32.36596039353566567 ) ) ;
#867=DIRECTION ( 'NONE',  ( 0.000000000000000000, 0.000000000000000000, 1.000000000000000000 ) ) ;
#872=CARTESIAN_POINT ( 'NONE',  ( -6.869994990996020512, 8.320472135496153183E-07, 17.65096039353565160 ) ) ;
#885=CARTESIAN_POINT ( 'NONE',  ( 13.48444335778406078, 4.726288251406393748, 37.73272338279511473 ) ) ;
#888=CIRCLE ( 'NONE', #1348, 3.573749999999999538 ) ;
#895=DIRECTION ( 'NONE',  ( -1.000000000000000000, -1.076498916035107621E-16, 0.000000000000000000 ) ) ;
#898=CARTESIAN_POINT ( 'NONE',  ( -7.619994990996019624, 8.320472136303528048E-07, 32.36596039353566567 ) ) ;
#899=VECTOR ( 'NONE', #1250, 1000.000000000000000 ) ;
#900=EDGE_CURVE ( 'NONE', #2669, #1336, #234, .T. ) ;
#904=ORIENTED_EDGE ( 'NONE', *, *, #3945, .F. ) ;
#905=CARTESIAN_POINT ( 'NONE',  ( 8.370005009003978813, -7.147499167952784838, 18.40096039353565160 ) ) ;
#913=DIRECTION ( 'NONE',  ( -1.000000000000000000, 1.076498916035107744E-16, 0.000000000000000000 ) ) ;
#914=STYLED_ITEM ( 'NONE', ( #1109 ), #1920 ) ;
#915=VECTOR ( 'NONE', #3007, 1000.000000000000000 ) ;
#919=VERTEX_POINT ( 'NONE', #4627 ) ;
#920=LINE ( 'NONE', #561, #1310 ) ;
#922=LINE ( 'NONE', #4522, #4502 ) ;
#924=CARTESIAN_POINT ( 'NONE',  ( 7.620005009003980589, -6.397499167952786614, 18.40096039353565160 ) ) ;
#925=ADVANCED_FACE ( 'NONE', ( #4198 ), #2105, .T. ) ;
#935=PLANE ( 'NONE',  #3809 ) ;
#937=EDGE_LOOP ( 'NONE', ( #2882, #2819, #1887, #4599 ) ) ;
#938=B_SPLINE_CURVE_WITH_KNOTS ( 'NONE', 3,
 ( #622, #3889, #668, #2735, #597, #4625, #4175, #958, #4579, #1339, #2104, #2064, #640, #224, #2756, #4197, #2394, #318, #1675, #1739, #2019, #3843, #1411, #1365 ),
 .UNSPECIFIED., .F., .F.,
 ( 4, 2, 2, 2, 2, 2, 2, 2, 2, 2, 2, 4 ),
 ( -0.01136693575711653602, -0.009946068787476960993, -0.008525201817837385967, -0.007104334848197810942, -0.006393901363378032103, -0.005683467878558252397, -0.004973034393738473558, -0.004262600908918695586, -0.002841733939279125765, -0.002131300454459342589, -0.001420866969639559413, 8.673617379884035472E-18 ),
 .UNSPECIFIED. ) ;
#948=ORIENTED_EDGE ( 'NONE', *, *, #4023, .F. ) ;
#951=EDGE_CURVE ( 'NONE', #1336, #230, #3440, .T. ) ;
#952=VERTEX_POINT ( 'NONE', #2782 ) ;
#953=CARTESIAN_POINT ( 'NONE',  ( -8.369994990996016071, 6.397500832047212427, 18.40096039353565160 ) ) ;
#958=CARTESIAN_POINT ( 'NONE',  ( -13.05597643801425711, -5.804668947475532192, 36.54283959188024511 ) ) ;
#959=DIRECTION ( 'NONE',  ( 0.000000000000000000, 0.000000000000000000, 1.000000000000000000 ) ) ;
#962=CARTESIAN_POINT ( 'NONE',  ( 14.12144740918446395, -2.180874814963778885, 35.20680156843862108 ) ) ;
#964=LINE ( 'NONE', #2425, #1946 ) ;
#966=CARTESIAN_POINT ( 'NONE',  ( -12.51136893239551640, 6.899599441734563854, 34.24694080209222591 ) ) ;
#972=EDGE_LOOP ( 'NONE', ( #2885, #1987, #262, #4171 ) ) ;
#977=FACE_BOUND ( 'NONE', #335, .T. ) ;
#980=CARTESIAN_POINT ( 'NONE',  ( 14.24237576372499170, -1.155158225338516198, 35.75590635509291104 ) ) ;
#982=EDGE_LOOP ( 'NONE', ( #3300, #3304, #664, #807, #4337 ) ) ;
#986=ORIENTED_EDGE ( 'NONE', *, *, #4578, .F. ) ;
#987=VECTOR ( 'NONE', #1300, 1000.000000000000000 ) ;
#988=DIRECTION ( 'NONE',  ( -0.000000000000000000, -0.000000000000000000, -1.000000000000000000 ) ) ;
#993=EDGE_CURVE ( 'NONE', #3784, #3671, #2297, .T. ) ;
#998=CARTESIAN_POINT ( 'NONE',  ( 12.37117714425455084, 7.147500832047210650, 18.29228486772272078 ) ) ;
#999=CARTESIAN_POINT ( 'NONE',  ( -17.48249499099600968, -7.897499167952782173, 18.40096039353565160 ) ) ;
#1005=SHAPE_REPRESENTATION ( 'Part 130_Varsay\X2\0131\X0\lan', ( #4483 ), #2891 ) ;
#1008=ORIENTED_EDGE ( 'NONE', *, *, #72, .T. ) ;
#1009=ADVANCED_FACE ( 'NONE', ( #3614 ), #3267, .T. ) ;
#1016=ADVANCED_FACE ( 'NONE', ( #68 ), #93, .F. ) ;
#1018=ORIENTED_EDGE ( 'NONE', *, *, #3857, .T. ) ;
#1019=CARTESIAN_POINT ( 'NONE',  ( -8.369994990996019624, -7.147499167952783061, 18.40096039353565160 ) ) ;
#1027=LINE ( 'NONE', #1741, #592 ) ;
#1029=DIRECTION ( 'NONE',  ( 1.000000000000000000, 0.000000000000000000, 0.000000000000000000 ) ) ;
#1032=CARTESIAN_POINT ( 'NONE',  ( -12.13219476556017540, -7.546706554720789661, 17.73167833386939307 ) ) ;
#1035=LINE ( 'NONE', #3418, #2114 ) ;
#1043=VECTOR ( 'NONE', #427, 1000.000000000000000 ) ;
#1045=DIRECTION ( 'NONE',  ( 1.000000000000000000, -1.076498916035107744E-16, 0.000000000000000000 ) ) ;
#1047=B_SPLINE_CURVE_WITH_KNOTS ( 'NONE', 3,
 ( #3336, #1554, #4417, #1205, #156, #2624, #2272, #2196, #1850, #4293 ),
 .UNSPECIFIED., .F., .F.,
 ( 4, 2, 2, 2, 4 ),
 ( 0.000000000000000000, 0.0003199342119934981852, 0.0006398684239869963705, 0.0009598026359804945557, 0.001279736847973992741 ),
 .UNSPECIFIED. ) ;
#1051=CARTESIAN_POINT ( 'NONE',  ( 13.86256568255526034, -3.458942830591085205, 31.43753846713071809 ) ) ;
#1052=LINE ( 'NONE', #642, #2994 ) ;
#1054=CARTESIAN_POINT ( 'NONE',  ( -14.09196727617781164, -2.361570152882583873, 29.67356755769036880 ) ) ;
#1064=ORIENTED_EDGE ( 'NONE', *, *, #993, .F. ) ;
#1069=AXIS2_PLACEMENT_3D ( 'NONE', #855, #1198, #2592 ) ;
#1070=ADVANCED_FACE ( 'NONE', ( #1087 ), #721, .T. ) ;
#1071=ORIENTED_EDGE ( 'NONE', *, *, #743, .F. ) ;
#1072=CARTESIAN_POINT ( 'NONE',  ( 11.90639614989969886, 7.897500832047208874, 17.65096039353565160 ) ) ;
#1075=PRODUCT_CONTEXT ( 'NONE', #1115, 'mechanical' ) ;
#1076=CARTESIAN_POINT ( 'NONE',  ( -13.11668702015748345, 5.666584765013171321, 36.72824904517413103 ) ) ;
#1077=LINE ( 'NONE', #2219, #2407 ) ;
#1078=CARTESIAN_POINT ( 'NONE',  ( 14.20094901052502934, -1.585078670707976922, 29.15451588337786859 ) ) ;
#1083=LINE ( 'NONE', #3766, #2773 ) ;
#1084=ORIENTED_EDGE ( 'NONE', *, *, #747, .T. ) ;
#1085=DIRECTION ( 'NONE',  ( -1.000000000000000000, 1.076498916035107621E-16, 0.000000000000000000 ) ) ;
#1086=CIRCLE ( 'NONE', #1167, 0.7500000000000006661 ) ;
#1087=FACE_OUTER_BOUND ( 'NONE', #1448, .T. ) ;
#1091=EDGE_CURVE ( 'NONE', #952, #919, #1294, .T. ) ;
#1097=LINE ( 'NONE', #3960, #1525 ) ;
#1099=ADVANCED_FACE ( 'NONE', ( #2528 ), #1886, .F. ) ;
#1104=CARTESIAN_POINT ( 'NONE',  ( -3.749994990996019961, -3.749999167952787094, 3.790960393535649064 ) ) ;
#1109=PRESENTATION_STYLE_ASSIGNMENT (( #4324 ) ) ;
#1111=TOROIDAL_SURFACE ( 'NONE', #572, 1.500000000000000000, 0.7500000000000000000 ) ;
#1113=CARTESIAN_POINT ( 'NONE',  ( 14.03248876714921778, 2.692596214963125512, 34.72730100679951448 ) ) ;
#1114=DIRECTION ( 'NONE',  ( 0.000000000000000000, -1.000000000000000000, 0.000000000000000000 ) ) ;
#1115=APPLICATION_CONTEXT ( 'automotive_design' ) ;
#1116=B_SPLINE_CURVE_WITH_KNOTS ( 'NONE', 3,
 ( #4017, #351, #4398, #2601, #1489, #397, #1113, #789, #2930, #4327, #3947, #2502, #3221, #720, #2159, #3996 ),
 .UNSPECIFIED., .F., .F.,
 ( 4, 2, 2, 2, 2, 2, 2, 4 ),
 ( 0.01121777374642162449, 0.01261988060185674672, 0.01332093402957430783, 0.01402198745729186895, 0.01472304088500943006, 0.01542409431272699118, 0.01612514774044455229, 0.01682620116816211167 ),
 .UNSPECIFIED. ) ;
#1117=CARTESIAN_POINT ( 'NONE',  ( 5.009003980371977336E-06, 8.320472128100606877E-07, 3.790960393535649064 ) ) ;
#1118=AXIS2_PLACEMENT_3D ( 'NONE', #3853, #1689, #3533 ) ;
#1120=ORIENTED_EDGE ( 'NONE', *, *, #1171, .T. ) ;
#1123=ORIENTED_EDGE ( 'NONE', *, *, #3319, .T. ) ;
#1130=CARTESIAN_POINT ( 'NONE',  ( -14.28158997014890375, 0.4709339481348280287, 28.81561122639583417 ) ) ;
#1131=CARTESIAN_POINT ( 'NONE',  ( -12.30671192345078957, -7.258092364145180220, 17.99507373849870007 ) ) ;
#1132=VECTOR ( 'NONE', #1533, 1000.000000000000000 ) ;
#1136=VECTOR ( 'NONE', #2985, 1000.000000000000000 ) ;
#1139=CARTESIAN_POINT ( 'NONE',  ( 7.620005009003978813, 8.320472119897684647E-07, 32.36596039353566567 ) ) ;
#1143=VERTEX_POINT ( 'NONE', #1233 ) ;
#1144=ORIENTED_EDGE ( 'NONE', *, *, #1792, .T. ) ;
#1150=AXIS2_PLACEMENT_3D ( 'NONE', #3611, #2874, #1830 ) ;
#1151=CARTESIAN_POINT ( 'NONE',  ( 5.009003980371977336E-06, 3.750000832047212906, 3.790960393535649064 ) ) ;
#1158=CYLINDRICAL_SURFACE ( 'NONE', #3129, 14.28750000000000142 ) ;
#1162=CARTESIAN_POINT ( 'NONE',  ( 7.620005009003977037, 12.08587093932537826, 18.40096039353565160 ) ) ;
#1164=CARTESIAN_POINT ( 'NONE',  ( 8.370005009003978813, 6.397500832047211539, 17.65096039353565160 ) ) ;
#1167=AXIS2_PLACEMENT_3D ( 'NONE', #115, #2979, #2294 ) ;
#1171=EDGE_CURVE ( 'NONE', #724, #2363, #1982, .T. ) ;
#1173=ORIENTED_EDGE ( 'NONE', *, *, #3501, .T. ) ;
#1174=EDGE_CURVE ( 'NONE', #4479, #2091, #212, .T. ) ;
#1177=LINE ( 'NONE', #3013, #3692 ) ;
#1186=LINE ( 'NONE', #45, #3815 ) ;
#1187=CIRCLE ( 'NONE', #119, 0.7500000000000006661 ) ;
#1189=ORIENTED_EDGE ( 'NONE', *, *, #951, .F. ) ;
#1197=CARTESIAN_POINT ( 'NONE',  ( 13.83333314027810701, 3.573750832047210668, 32.36596039353566567 ) ) ;
#1198=DIRECTION ( 'NONE',  ( 1.000000000000000000, -0.000000000000000000, 0.000000000000000000 ) ) ;
#1202=SHAPE_REPRESENTATION_RELATIONSHIP ( 'NONE' , 'NONE' ,  #1005, #161 ) ;
#1205=CARTESIAN_POINT ( 'NONE',  ( -12.30737647472887630, 7.256961385541304210, 17.99723211794410460 ) ) ;
#1208=VERTEX_POINT ( 'NONE', #4137 ) ;
#1210=PLANE ( 'NONE',  #4039 ) ;
#1212=VERTEX_POINT ( 'NONE', #583 ) ;
#1219=CARTESIAN_POINT ( 'NONE',  ( 14.17557912141665888, 1.795475159085173189, 29.26726773362641509 ) ) ;
#1221=B_SPLINE_CURVE_WITH_KNOTS ( 'NONE', 3,
 ( #1072, #1760, #1521, #2801, #2443, #360, #2465, #337, #998, #1805 ),
 .UNSPECIFIED., .F., .F.,
 ( 4, 2, 2, 2, 4 ),
 ( 0.000000000000000000, 0.0003186827706029872194, 0.0006373655412059744388, 0.0009560483118089616039, 0.001274731082411948878 ),
 .UNSPECIFIED. ) ;
#1222=CIRCLE ( 'NONE', #87, 0.7500000000000006661 ) ;
#1223=ORIENTED_EDGE ( 'NONE', *, *, #2098, .F. ) ;
#1225=PLANE ( 'NONE',  #3529 ) ;
#1228=CARTESIAN_POINT ( 'NONE',  ( -3.749994990996019961, -3.749999167952787094, 18.79096039353565217 ) ) ;
#1233=CARTESIAN_POINT ( 'NONE',  ( -11.90638613189173789, 7.897500832047212427, 17.65096039353565160 ) ) ;
#1234=FACE_OUTER_BOUND ( 'NONE', #2903, .T. ) ;
#1235=ORIENTED_EDGE ( 'NONE', *, *, #2327, .F. ) ;
#1239=DIRECTION ( 'NONE',  ( 1.000000000000000000, -1.076498916035107621E-16, -0.000000000000000000 ) ) ;
#1240=EDGE_CURVE ( 'NONE', #4527, #1779, #616, .T. ) ;
#1241=EDGE_LOOP ( 'NONE', ( #3624, #1709, #1817, #495 ) ) ;
#1242=ORIENTED_EDGE ( 'NONE', *, *, #280, .F. ) ;
#1245=ORIENTED_EDGE ( 'NONE', *, *, #3244, .F. ) ;
#1246=FACE_OUTER_BOUND ( 'NONE', #3398, .T. ) ;
#1247=EDGE_CURVE ( 'NONE', #2845, #3903, #920, .T. ) ;
#1250=DIRECTION ( 'NONE',  ( -8.673617379884035472E-17, -1.000000000000000000, 0.000000000000000000 ) ) ;
#1251=CARTESIAN_POINT ( 'NONE',  ( 13.11703476964942361, 5.665799994185183763, 36.72925822850186250 ) ) ;
#1273=CARTESIAN_POINT ( 'NONE',  ( -3.749994990996019517, 3.750000832047212906, 18.79096039353565217 ) ) ;
#1276=EDGE_CURVE ( 'NONE', #1617, #2188, #1580, .T. ) ;
#1282=B_SPLINE_CURVE_WITH_KNOTS ( 'NONE', 3,
 ( #3720, #2324, #3772, #1646, #3062, #4148, #1547, #2240, #3674, #450, #1898, #3329, #452, #1076, #2493, #2197, #1684, #3104, #4541, #966, #857, #2265, #2991, #4392 ),
 .UNSPECIFIED., .F., .F.,
 ( 4, 2, 2, 2, 2, 2, 2, 2, 2, 2, 2, 4 ),
 ( 8.239936510889833698E-18, 0.001420502804142420540, 0.002841005608284832840, 0.004261508412427245790, 0.004971759814498445326, 0.005682011216569644863, 0.006392262618640844399, 0.007102514020712043935, 0.008523016824854427395, 0.009233268226925630401, 0.009943519628996829937, 0.01136402243313925156 ),
 .UNSPECIFIED. ) ;
#1294=CIRCLE ( 'NONE', #18, 0.7500000000000006661 ) ;
#1299=CARTESIAN_POINT ( 'NONE',  ( 13.23943158335225334, 5.373578213064656772, 37.08446802545930154 ) ) ;
#1300=DIRECTION ( 'NONE',  ( 0.000000000000000000, 0.000000000000000000, -1.000000000000000000 ) ) ;
#1309=ORIENTED_EDGE ( 'NONE', *, *, #3374, .T. ) ;
#1310=VECTOR ( 'NONE', #2340, 1000.000000000000000 ) ;
#1314=EDGE_LOOP ( 'NONE', ( #4261, #1144, #4001, #2511, #3951, #2766, #1545, #515, #2165, #2082, #3629, #3382, #4056, #1242, #4569, #1319 ) ) ;
#1315=EDGE_LOOP ( 'NONE', ( #1633, #2629, #486, #2058 ) ) ;
#1317=DIRECTION ( 'NONE',  ( -0.000000000000000000, -0.000000000000000000, -1.000000000000000000 ) ) ;
#1319=ORIENTED_EDGE ( 'NONE', *, *, #375, .F. ) ;
#1320=AXIS2_PLACEMENT_3D ( 'NONE', #3949, #3998, #2562 ) ;
#1322=CARTESIAN_POINT ( 'NONE',  ( -14.12110210206280136, -2.183034303507356277, 35.20514053939854904 ) ) ;
#1323=CARTESIAN_POINT ( 'NONE',  ( 13.42337887132440066, -4.896491311848273575, 37.57783078324375481 ) ) ;
#1325=CARTESIAN_POINT ( 'NONE',  ( -14.26312271147663502, -0.9396272187553439403, 28.88658383315958389 ) ) ;
#1326=DIRECTION ( 'NONE',  ( -1.000000000000000000, 1.076498916035107744E-16, 0.000000000000000000 ) ) ;
#1328=ORIENTED_EDGE ( 'NONE', *, *, #233, .F. ) ;
#1336=VERTEX_POINT ( 'NONE', #2111 ) ;
#1339=CARTESIAN_POINT ( 'NONE',  ( -13.23942156534429415, -5.373576548970228295, 37.08446802545930154 ) ) ;
#1345=ORIENTED_EDGE ( 'NONE', *, *, #2186, .T. ) ;
#1347=LINE ( 'NONE', #192, #3912 ) ;
#1348=AXIS2_PLACEMENT_3D ( 'NONE', #1139, #418, #2883 ) ;
#1349=EDGE_CURVE ( 'NONE', #3252, #2304, #1397, .T. ) ;
#1352=DIRECTION ( 'NONE',  ( -1.000000000000000000, 1.076498916035107744E-16, 0.000000000000000000 ) ) ;
#1356=ORIENTED_EDGE ( 'NONE', *, *, #120, .T. ) ;
#1360=VECTOR ( 'NONE', #1429, 1000.000000000000000 ) ;
#1365=CARTESIAN_POINT ( 'NONE',  ( -14.28749499099602005, 8.320472128100606877E-07, 39.51346039353565942 ) ) ;
#1366=CARTESIAN_POINT ( 'NONE',  ( 12.76994908703544418, -6.411093920557875414, 35.55968826673669980 ) ) ;
#1372=AXIS2_PLACEMENT_3D ( 'NONE', #4346, #1467, #1485 ) ;
#1389=FACE_OUTER_BOUND ( 'NONE', #1527, .T. ) ;
#1391=DIRECTION ( 'NONE',  ( -1.000000000000000000, -0.000000000000000000, -0.000000000000000000 ) ) ;
#1394=CARTESIAN_POINT ( 'NONE',  ( 13.92261115689014694, -3.209696657368923400, 33.95459613213026984 ) ) ;
#1397=LINE ( 'NONE', #628, #301 ) ;
#1406=ORIENTED_EDGE ( 'NONE', *, *, #3488, .F. ) ;
#1411=CARTESIAN_POINT ( 'NONE',  ( -14.28749499099602005, -0.4809632029028111933, 39.51346039353565232 ) ) ;
#1413=CARTESIAN_POINT ( 'NONE',  ( 8.370005009003978813, 6.397500832047211539, 18.40096039353565160 ) ) ;
#1415=CARTESIAN_POINT ( 'NONE',  ( -14.03274346603649647, -2.691220199277232883, 30.00305411948872703 ) ) ;
#1419=DIRECTION ( 'NONE',  ( 0.000000000000000000, 0.000000000000000000, -1.000000000000000000 ) ) ;
#1420=B_SPLINE_CURVE_WITH_KNOTS ( 'NONE', 3,
 ( #3878, #1511, #3243, #415, #3270, #1861, #3969, #4396, #19, #1535 ),
 .UNSPECIFIED., .F., .F.,
 ( 4, 2, 2, 2, 4 ),
 ( 0.000000000000000000, 0.0003199342119934985105, 0.0006398684239869970210, 0.0009598026359804955315, 0.001279736847973994042 ),
 .UNSPECIFIED. ) ;
#1425=AXIS2_PLACEMENT_3D ( 'NONE', #3572, #22, #1470 ) ;
#1427=EDGE_LOOP ( 'NONE', ( #4075, #4081, #986, #3437, #4420, #723, #3100, #3832, #4212, #4478, #3643, #4231, #3504, #2488, #1064, #3714 ) ) ;
#1429=DIRECTION ( 'NONE',  ( -0.000000000000000000, -0.000000000000000000, -1.000000000000000000 ) ) ;
#1430=EDGE_LOOP ( 'NONE', ( #1309, #1008, #2741, #3697 ) ) ;
#1437=LINE ( 'NONE', #1878, #4025 ) ;
#1441=ORIENTED_EDGE ( 'NONE', *, *, #1240, .F. ) ;
#1448=EDGE_LOOP ( 'NONE', ( #2124, #3685, #551, #2099 ) ) ;
#1454=ADVANCED_FACE ( 'NONE', ( #2154 ), #15, .F. ) ;
#1458=AXIS2_PLACEMENT_3D ( 'NONE', #2978, #4519, #3712 ) ;
#1461=CARTESIAN_POINT ( 'NONE',  ( 14.28750500900398279, -0.2342234701874567893, 28.79221039353567235 ) ) ;
#1465=CARTESIAN_POINT ( 'NONE',  ( 14.28750500900398279, 8.320472145597748469E-07, 28.79221039353566880 ) ) ;
#1466=CARTESIAN_POINT ( 'NONE',  ( 14.99250500900398109, 7.897500832047208874, 18.40096039353565160 ) ) ;
#1467=DIRECTION ( 'NONE',  ( 1.076498916035107621E-16, 1.000000000000000000, -0.000000000000000000 ) ) ;
#1468=LINE ( 'NONE', #1162, #49 ) ;
#1470=DIRECTION ( 'NONE',  ( 0.000000000000000000, 1.000000000000000000, 0.000000000000000000 ) ) ;
#1474=ORIENTED_EDGE ( 'NONE', *, *, #601, .T. ) ;
#1477=ORIENTED_EDGE ( 'NONE', *, *, #2401, .T. ) ;
#1482=CARTESIAN_POINT ( 'NONE',  ( -14.09217544079672280, 2.360382569825107968, 29.67243804805142204 ) ) ;
#1483=DIRECTION ( 'NONE',  ( 1.000000000000000000, 0.000000000000000000, 0.000000000000000000 ) ) ;
#1485=DIRECTION ( 'NONE',  ( -1.000000000000000000, 0.000000000000000000, 0.000000000000000000 ) ) ;
#1488=VERTEX_POINT ( 'NONE', #3635 ) ;
#1489=CARTESIAN_POINT ( 'NONE',  ( 13.94789236355132545, 3.099469737325899032, 34.16023755992365096 ) ) ;
#1495=ADVANCED_FACE ( 'NONE', ( #2878, #3966 ), #2522, .F. ) ;
#1497=VERTEX_POINT ( 'NONE', #2901 ) ;
#1499=CARTESIAN_POINT ( 'NONE',  ( -14.28159601362361286, 0.4702588884268389391, 35.91633004324798861 ) ) ;
#1503=CARTESIAN_POINT ( 'NONE',  ( 14.09194676216336362, -2.361710026607503288, 29.67376555440869268 ) ) ;
#1504=CARTESIAN_POINT ( 'NONE',  ( -14.20092530083940296, 1.585302497639503372, 29.15456951301168331 ) ) ;
#1505=DIRECTION ( 'NONE',  ( 0.000000000000000000, 0.000000000000000000, 1.000000000000000000 ) ) ;
#1506=CIRCLE ( 'NONE', #4125, 0.7500000000000006661 ) ;
#1510=DIRECTION ( 'NONE',  ( 0.000000000000000000, -0.000000000000000000, 1.000000000000000000 ) ) ;
#1511=CARTESIAN_POINT ( 'NONE',  ( 12.37117714425454551, -7.147499167952783949, 18.29267992112417929 ) ) ;
#1515=CARTESIAN_POINT ( 'NONE',  ( 8.370005009003978813, -6.397499167952784838, 3.790960393535648176 ) ) ;
#1519=DIRECTION ( 'NONE',  ( -1.355782318074878530E-16, 1.000000000000000000, 0.000000000000000000 ) ) ;
#1521=CARTESIAN_POINT ( 'NONE',  ( 12.02320160177486486, 7.719185208846096380, 17.66665972527255235 ) ) ;
#1522=DIRECTION ( 'NONE',  ( 0.000000000000000000, 0.000000000000000000, 1.000000000000000000 ) ) ;
#1525=VECTOR ( 'NONE', #4008, 1000.000000000000000 ) ;
#1527=EDGE_LOOP ( 'NONE', ( #3204, #2534, #4147, #1591 ) ) ;
#1529=CARTESIAN_POINT ( 'NONE',  ( -14.25914032423990818, 0.9284644955993464066, 35.82489411863820550 ) ) ;
#1531=ORIENTED_EDGE ( 'NONE', *, *, #3244, .T. ) ;
#1532=DIRECTION ( 'NONE',  ( -1.000000000000000000, 1.076498916035107744E-16, 0.000000000000000000 ) ) ;
#1533=DIRECTION ( 'NONE',  ( -1.000000000000000000, 1.076498916035107744E-16, 0.000000000000000000 ) ) ;
#1535=CARTESIAN_POINT ( 'NONE',  ( 11.90639614989970063, -7.897499167952783949, 17.65096039353565160 ) ) ;
#1538=ORIENTED_EDGE ( 'NONE', *, *, #3906, .T. ) ;
#1539=CARTESIAN_POINT ( 'NONE',  ( 3.750005009003979595, 3.750000832047212906, 3.790960393535649064 ) ) ;
#1540=DIRECTION ( 'NONE',  ( 0.000000000000000000, 1.000000000000000000, 0.000000000000000000 ) ) ;
#1541=EDGE_LOOP ( 'NONE', ( #1356, #2889, #184, #1245 ) ) ;
#1543=CARTESIAN_POINT ( 'NONE',  ( 5.009003980371977336E-06, 8.320472128100606877E-07, 17.65096039353565160 ) ) ;
#1545=ORIENTED_EDGE ( 'NONE', *, *, #2855, .F. ) ;
#1547=CARTESIAN_POINT ( 'NONE',  ( -13.83078033805465878, 3.606002719002763257, 38.55461960823348022 ) ) ;
#1552=CYLINDRICAL_SURFACE ( 'NONE', #2314, 7.147499999999999076 ) ;
#1554=CARTESIAN_POINT ( 'NONE',  ( -12.37116712624658277, 7.147500832047212427, 18.29267992112417929 ) ) ;
#1570=CARTESIAN_POINT ( 'NONE',  ( 7.620005009003978813, -3.573749167952787520, 32.36596039353566567 ) ) ;
#1573=FACE_OUTER_BOUND ( 'NONE', #1541, .T. ) ;
#1579=LINE ( 'NONE', #487, #3590 ) ;
#1580=LINE ( 'NONE', #2426, #3695 ) ;
#1582=EDGE_CURVE ( 'NONE', #2669, #4497, #3659, .T. ) ;
#1584=ORIENTED_EDGE ( 'NONE', *, *, #84, .F. ) ;
#1585=CARTESIAN_POINT ( 'NONE',  ( 6.870005009003977925, 6.397500832047211539, 18.40096039353565160 ) ) ;
#1590=EDGE_CURVE ( 'NONE', #2828, #724, #811, .T. ) ;
#1591=ORIENTED_EDGE ( 'NONE', *, *, #3150, .T. ) ;
#1592=VERTEX_POINT ( 'NONE', #4489 ) ;
#1593=CARTESIAN_POINT ( 'NONE',  ( 13.94792677495786570, 3.099290160580272069, 30.57149645866954657 ) ) ;
#1596=ADVANCED_FACE ( 'NONE', ( #4463 ), #1225, .F. ) ;
#1598=ORIENTED_EDGE ( 'NONE', *, *, #1171, .F. ) ;
#1600=DIRECTION ( 'NONE',  ( 0.000000000000000000, 1.000000000000000000, 0.000000000000000000 ) ) ;
#1606=FACE_OUTER_BOUND ( 'NONE', #3085, .T. ) ;
#1610=CARTESIAN_POINT ( 'NONE',  ( -8.369994990996019624, -6.397499167952784838, 17.65096039353565160 ) ) ;
#1613=PRODUCT_DEFINITION_CONTEXT ( 'detailed design', #2779, 'design' ) ;
#1617=VERTEX_POINT ( 'NONE', #1995 ) ;
#1619=DIRECTION ( 'NONE',  ( -0.000000000000000000, -0.000000000000000000, 1.000000000000000000 ) ) ;
#1629=FACE_OUTER_BOUND ( 'NONE', #570, .T. ) ;
#1633=ORIENTED_EDGE ( 'NONE', *, *, #2504, .F. ) ;
#1635=CARTESIAN_POINT ( 'NONE',  ( -8.369994990996019624, -6.397499167952784838, 18.40096039353565160 ) ) ;
#1646=CARTESIAN_POINT ( 'NONE',  ( -14.17127809776796532, 1.877062544604579664, 39.27869980365569091 ) ) ;
#1654=CARTESIAN_POINT ( 'NONE',  ( 13.83082084157986458, 3.605824707096489501, 38.55467339862568110 ) ) ;
#1655=LINE ( 'NONE', #4514, #987 ) ;
#1656=CARTESIAN_POINT ( 'NONE',  ( 14.20084204937985994, -1.586109036619252288, 35.57693867976828983 ) ) ;
#1660=DIRECTION ( 'NONE',  ( 8.673617379884035472E-17, 1.000000000000000000, -0.000000000000000000 ) ) ;
#1662=ORIENTED_EDGE ( 'NONE', *, *, #4330, .T. ) ;
#1673=AXIS2_PLACEMENT_3D ( 'NONE', #3141, #341, #3480 ) ;
#1675=CARTESIAN_POINT ( 'NONE',  ( -14.09722260588723408, -2.335208591167885039, 39.12537387803049427 ) ) ;
#1684=CARTESIAN_POINT ( 'NONE',  ( -12.76993906902747611, 6.411095584652301227, 35.55968826673666427 ) ) ;
#1685=CIRCLE ( 'NONE', #3842, 3.573749999999999538 ) ;
#1689=DIRECTION ( 'NONE',  ( -1.000000000000000000, 1.076498916035107744E-16, 0.000000000000000000 ) ) ;
#1691=ORIENTED_EDGE ( 'NONE', *, *, #527, .T. ) ;
#1693=ORIENTED_EDGE ( 'NONE', *, *, #3936, .T. ) ;
#1695=CIRCLE ( 'NONE', #28, 6.397499999999999964 ) ;
#1697=CARTESIAN_POINT ( 'NONE',  ( 12.87888030253338556, -6.192545380470082073, 35.96503381882251205 ) ) ;
#1709=ORIENTED_EDGE ( 'NONE', *, *, #2190, .F. ) ;
#1714=DIRECTION ( 'NONE',  ( -1.000000000000000000, 1.076498916035107621E-16, 0.000000000000000000 ) ) ;
#1717=CARTESIAN_POINT ( 'NONE',  ( 12.37117714425454551, -7.147499167952786614, 32.36596039353565857 ) ) ;
#1722=DIRECTION ( 'NONE',  ( -1.000000000000000000, 1.076498916035107621E-16, 0.000000000000000000 ) ) ;
#1724=CARTESIAN_POINT ( 'NONE',  ( -13.83332312227014782, 3.573750832047214665, 32.60017139658542362 ) ) ;
#1725=AXIS2_PLACEMENT_3D ( 'NONE', #4602, #1714, #3137 ) ;
#1726=ADVANCED_FACE ( 'NONE', ( #1974 ), #1552, .T. ) ;
#1729=VERTEX_POINT ( 'NONE', #3379 ) ;
#1739=CARTESIAN_POINT ( 'NONE',  ( -14.16478064111921320, -1.882517949369861610, 39.26516300994397568 ) ) ;
#1740=CARTESIAN_POINT ( 'NONE',  ( 12.51137895040347736, -6.899597777640140706, 34.24694080209222591 ) ) ;
#1741=CARTESIAN_POINT ( 'NONE',  ( 14.28750500900398279, 8.320472145597748469E-07, 17.65096039353565160 ) ) ;
#1742=ADVANCED_FACE ( 'NONE', ( #1389, #977 ), #3166, .F. ) ;
#1744=DIRECTION ( 'NONE',  ( -1.000000000000000000, 0.000000000000000000, 0.000000000000000000 ) ) ;
#1749=LINE ( 'NONE', #349, #4366 ) ;
#1755=CARTESIAN_POINT ( 'NONE',  ( -14.28749499099602005, 8.320472117659611842E-07, 35.93971039353566255 ) ) ;
#1760=CARTESIAN_POINT ( 'NONE',  ( 11.96611785441004372, 7.807463481809645778, 17.65096039353565160 ) ) ;
#1761=ORIENTED_EDGE ( 'NONE', *, *, #2051, .F. ) ;
#1763=EDGE_CURVE ( 'NONE', #209, #3059, #3468, .T. ) ;
#1764=DIRECTION ( 'NONE',  ( -1.076498916035107621E-16, 1.000000000000000000, 0.000000000000000000 ) ) ;
#1769=EDGE_CURVE ( 'NONE', #2126, #3808, #938, .T. ) ;
#1770=CARTESIAN_POINT ( 'NONE',  ( -14.00292873865404530, 2.840413803447212615, 30.18475356502192142 ) ) ;
#1771=CARTESIAN_POINT ( 'NONE',  ( -11.96610783640208631, -7.807461817715218189, 17.65096039353565160 ) ) ;
#1775=CARTESIAN_POINT ( 'NONE',  ( -8.369994990996016071, 7.897500832047212427, 17.65096039353565160 ) ) ;
#1779=VERTEX_POINT ( 'NONE', #2781 ) ;
#1781=FACE_OUTER_BOUND ( 'NONE', #972, .T. ) ;
#1785=CARTESIAN_POINT ( 'NONE',  ( 13.05554860573490572, -5.805646240973097783, 36.54145662508980763 ) ) ;
#1786=AXIS2_PLACEMENT_3D ( 'NONE', #760, #3655, #1532 ) ;
#1791=DIRECTION ( 'NONE',  ( -0.000000000000000000, -0.000000000000000000, -1.000000000000000000 ) ) ;
#1792=EDGE_CURVE ( 'NONE', #1336, #3535, #1027, .T. ) ;
#1796=DIRECTION ( 'NONE',  ( 0.000000000000000000, -1.000000000000000000, 0.000000000000000000 ) ) ;
#1797=AXIS2_PLACEMENT_3D ( 'NONE', #67, #1085, #1796 ) ;
#1799=EDGE_CURVE ( 'NONE', #2566, #919, #1052, .T. ) ;
#1801=ORIENTED_EDGE ( 'NONE', *, *, #900, .F. ) ;
#1802=ADVANCED_FACE ( 'NONE', ( #250 ), #669, .F. ) ;
#1804=ORIENTED_EDGE ( 'NONE', *, *, #2094, .F. ) ;
#1805=CARTESIAN_POINT ( 'NONE',  ( 12.37117714425454551, 7.147500832047207098, 18.40096039353565160 ) ) ;
#1811=CARTESIAN_POINT ( 'NONE',  ( 14.25915967094480585, -0.9287842060774819108, 28.90698488472980898 ) ) ;
#1817=ORIENTED_EDGE ( 'NONE', *, *, #1091, .F. ) ;
#1830=DIRECTION ( 'NONE',  ( 1.000000000000000000, 0.000000000000000000, 0.000000000000000000 ) ) ;
#1831=CARTESIAN_POINT ( 'NONE',  ( 12.37117714425454551, 7.147500832047207098, 18.40096039353565160 ) ) ;
#1832=AXIS2_PLACEMENT_3D ( 'NONE', #3884, #3837, #3447 ) ;
#1836=EDGE_CURVE ( 'NONE', #1947, #3411, #1506, .T. ) ;
#1838=( NAMED_UNIT ( * ) PLANE_ANGLE_UNIT ( ) SI_UNIT ( $, .RADIAN. ) );
#1842=DIRECTION ( 'NONE',  ( 1.000000000000000000, 0.000000000000000000, 0.000000000000000000 ) ) ;
#1845=ORIENTED_EDGE ( 'NONE', *, *, #1590, .F. ) ;
#1847=B_SPLINE_CURVE_WITH_KNOTS ( 'NONE', 3,
 ( #4162, #1771, #4251, #1032, #3550, #2452, #1131, #3589, #3613, #2546 ),
 .UNSPECIFIED., .F., .F.,
 ( 4, 2, 2, 2, 4 ),
 ( 0.000000000000000000, 0.0003186827706029867857, 0.0006373655412059735714, 0.0009560483118089603029, 0.001274731082411947143 ),
 .UNSPECIFIED. ) ;
#1850=CARTESIAN_POINT ( 'NONE',  ( -11.96599547592554025, 7.807632878173365043, 17.65096039353564805 ) ) ;
#1853=CARTESIAN_POINT ( 'NONE',  ( 14.03294480382409937, -2.690185271046441784, 30.00196167051755225 ) ) ;
#1857=DIRECTION ( 'NONE',  ( -0.000000000000000000, -0.000000000000000000, -1.000000000000000000 ) ) ;
#1859=DIRECTION ( 'NONE',  ( 0.000000000000000000, 0.000000000000000000, 1.000000000000000000 ) ) ;
#1861=CARTESIAN_POINT ( 'NONE',  ( 12.18357978802232289, -7.463262154146836913, 17.78165220884836728 ) ) ;
#1864=CARTESIAN_POINT ( 'NONE',  ( -3.749994990996019961, -3.749999167952787094, 3.790960393535649064 ) ) ;
#1867=EDGE_LOOP ( 'NONE', ( #3128, #228, #127, #3376 ) ) ;
#1871=DIRECTION ( 'NONE',  ( 9.517981353260378315E-33, 8.841607930564763213E-17, -1.000000000000000000 ) ) ;
#1872=CARTESIAN_POINT ( 'NONE',  ( 14.24248326661499497, 1.154100376730833544, 28.97554744807429117 ) ) ;
#1878=CARTESIAN_POINT ( 'NONE',  ( 12.37117714425454551, -7.147499167952784838, 17.65096039353565160 ) ) ;
#1882=SURFACE_SIDE_STYLE ('',( #2880 ) ) ;
#1885=DIRECTION ( 'NONE',  ( -0.000000000000000000, -0.000000000000000000, -1.000000000000000000 ) ) ;
#1886=CYLINDRICAL_SURFACE ( 'NONE', #3097, 0.7499999999999997780 ) ;
#1887=ORIENTED_EDGE ( 'NONE', *, *, #4573, .F. ) ;
#1888=CARTESIAN_POINT ( 'NONE',  ( 8.370005009003978813, -6.397499167952786614, 18.40096039353565160 ) ) ;
#1893=CIRCLE ( 'NONE', #2479, 0.7500000000000006661 ) ;
#1895=B_SPLINE_CURVE_WITH_KNOTS ( 'NONE', 3,
 ( #3963, #736, #4341, #2131, #2571, #2898, #2175, #1770, #2853, #1482, #60, #3567, #1504, #3917, #713, #1130, #672, #3939 ),
 .UNSPECIFIED., .F., .F.,
 ( 4, 2, 2, 2, 2, 2, 2, 2, 4 ),
 ( 0.005610428130223212191, 0.006311357680970753822, 0.007012287231718294586, 0.007713216782465835350, 0.008414146333213377849, 0.009115075883960918612, 0.009816005434708459376, 0.01051693498545600187, 0.01121786453620354437 ),
 .UNSPECIFIED. ) ;
#1898=CARTESIAN_POINT ( 'NONE',  ( -13.42336885331644147, 4.896492975942702053, 37.57783078324376191 ) ) ;
#1906=ORIENTED_EDGE ( 'NONE', *, *, #113, .T. ) ;
#1914=LINE ( 'NONE', #2256, #2932 ) ;
#1920=MANIFOLD_SOLID_BREP ( 'Ölçek1', #3278 ) ;
#1923=EDGE_CURVE ( 'NONE', #4497, #1497, #2326, .T. ) ;
#1924=DIRECTION ( 'NONE',  ( -8.673617379884035472E-17, -1.000000000000000000, 0.000000000000000000 ) ) ;
#1927=CARTESIAN_POINT ( 'NONE',  ( -7.619994990996019624, 8.320472136303528048E-07, 32.36596039353565857 ) ) ;
#1934=EDGE_CURVE ( 'NONE', #724, #4479, #108, .T. ) ;
#1946=VECTOR ( 'NONE', #325, 1000.000000000000000 ) ;
#1947=VERTEX_POINT ( 'NONE', #3019 ) ;
#1951=CARTESIAN_POINT ( 'NONE',  ( 12.87896032641104505, 6.192408470356285832, 35.96538579746960806 ) ) ;
#1958=CARTESIAN_POINT ( 'NONE',  ( 14.99250500900397753, 8.320472111961197689E-07, 32.36596039353565857 ) ) ;
#1960=CARTESIAN_POINT ( 'NONE',  ( -17.48249499099600968, -7.147499167952782173, 3.790960393535648176 ) ) ;
#1961=CARTESIAN_POINT ( 'NONE',  ( -13.94750601360946796, 3.101197589506698993, 34.15745705064754389 ) ) ;
#1965=CARTESIAN_POINT ( 'NONE',  ( -7.619994990996017847, 6.397500832047212427, 18.40096039353565160 ) ) ;
#1970=DIRECTION ( 'NONE',  ( -0.000000000000000000, -1.000000000000000000, -0.000000000000000000 ) ) ;
#1971=VECTOR ( 'NONE', #2221, 1000.000000000000000 ) ;
#1974=FACE_OUTER_BOUND ( 'NONE', #3051, .T. ) ;
#1982=LINE ( 'NONE', #2027, #839 ) ;
#1984=CARTESIAN_POINT ( 'NONE',  ( -8.369994990996019624, -6.397499167952783061, 3.790960393535648176 ) ) ;
#1987=ORIENTED_EDGE ( 'NONE', *, *, #429, .T. ) ;
#1989=CARTESIAN_POINT ( 'NONE',  ( 5.009003980371977336E-06, 3.750000832047212906, 17.65096039353565160 ) ) ;
#1995=CARTESIAN_POINT ( 'NONE',  ( 8.370005009003980589, -7.147499167952786614, 32.36596039353565857 ) ) ;
#1999=CARTESIAN_POINT ( 'NONE',  ( 13.86272383238697969, -3.458313573812046737, 33.29701817273350173 ) ) ;
#2008=DIRECTION ( 'NONE',  ( 1.000000000000000000, -0.000000000000000000, -0.000000000000000000 ) ) ;
#2014=VERTEX_POINT ( 'NONE', #3707 ) ;
#2019=CARTESIAN_POINT ( 'NONE',  ( -14.19372585200764014, -1.650818847648656940, 39.32424842390233977 ) ) ;
#2021=CARTESIAN_POINT ( 'NONE',  ( 14.28750500900398102, 0.4809648669972392265, 39.51346039353565232 ) ) ;
#2027=CARTESIAN_POINT ( 'NONE',  ( 5.009003980046716684E-06, -3.749999167952787538, 17.65096039353565160 ) ) ;
#2030=CARTESIAN_POINT ( 'NONE',  ( -14.28749499099602005, 8.320472117659611842E-07, 35.93971039353566255 ) ) ;
#2033=ORIENTED_EDGE ( 'NONE', *, *, #3116, .T. ) ;
#2034=ORIENTED_EDGE ( 'NONE', *, *, #748, .F. ) ;
#2037=ORIENTED_EDGE ( 'NONE', *, *, #2094, .T. ) ;
#2038=DIRECTION ( 'NONE',  ( 1.000000000000000000, 0.000000000000000000, 0.000000000000000000 ) ) ;
#2040=CARTESIAN_POINT ( 'NONE',  ( 8.370005009003978813, -6.397499167952786614, 18.40096039353565160 ) ) ;
#2043=CARTESIAN_POINT ( 'NONE',  ( 13.30084886853356707, -5.220167152536361321, 37.25360547957400570 ) ) ;
#2044=CARTESIAN_POINT ( 'NONE',  ( 8.370005009003978813, 7.897500832047212427, 18.40096039353565160 ) ) ;
#2051=EDGE_CURVE ( 'NONE', #2260, #1488, #3779, .T. ) ;
#2055=LINE ( 'NONE', #2366, #3134 ) ;
#2056=ORIENTED_EDGE ( 'NONE', *, *, #3152, .F. ) ;
#2058=ORIENTED_EDGE ( 'NONE', *, *, #62, .F. ) ;
#2063=FACE_OUTER_BOUND ( 'NONE', #26, .T. ) ;
#2064=CARTESIAN_POINT ( 'NONE',  ( -13.42355275005542303, -4.895986476802388410, 37.57830303755702062 ) ) ;
#2067=CARTESIAN_POINT ( 'NONE',  ( 14.03294512273307859, -2.690168477928161828, 34.72994684450105751 ) ) ;
#2071=CARTESIAN_POINT ( 'NONE',  ( 3.750005009003979595, -3.749999167952787538, 3.790960393535649064 ) ) ;
#2076=EDGE_CURVE ( 'NONE', #1729, #4385, #1655, .T. ) ;
#2079=EDGE_LOOP ( 'NONE', ( #2567, #3014, #4031, #2442 ) ) ;
#2080=EDGE_CURVE ( 'NONE', #3952, #1143, #1047, .T. ) ;
#2082=ORIENTED_EDGE ( 'NONE', *, *, #3999, .F. ) ;
#2091=VERTEX_POINT ( 'NONE', #2871 ) ;
#2094=EDGE_CURVE ( 'NONE', #2828, #2091, #2516, .T. ) ;
#2098=EDGE_CURVE ( 'NONE', #3403, #3411, #1097, .T. ) ;
#2099=ORIENTED_EDGE ( 'NONE', *, *, #3256, .T. ) ;
#2100=DIRECTION ( 'NONE',  ( 0.000000000000000000, 1.000000000000000000, 0.000000000000000000 ) ) ;
#2104=CARTESIAN_POINT ( 'NONE',  ( -13.30104869160269665, -5.219631826751473191, 37.25417504454090789 ) ) ;
#2105=CYLINDRICAL_SURFACE ( 'NONE', #1673, 0.7499999999999997780 ) ;
#2111=CARTESIAN_POINT ( 'NONE',  ( 14.28750500900398279, 8.320472145597748469E-07, 39.51346039353565942 ) ) ;
#2114=VECTOR ( 'NONE', #695, 1000.000000000000000 ) ;
#2117=DIRECTION ( 'NONE',  ( 1.000000000000000000, -1.076498916035107621E-16, -0.000000000000000000 ) ) ;
#2118=PRODUCT_DEFINITION_SHAPE ( 'NONE', 'NONE',  #500 ) ;
#2122=EDGE_CURVE ( 'NONE', #3671, #2770, #3956, .T. ) ;
#2124=ORIENTED_EDGE ( 'NONE', *, *, #1247, .F. ) ;
#2126=VERTEX_POINT ( 'NONE', #2708 ) ;
#2127=CARTESIAN_POINT ( 'NONE',  ( 11.90639614989970063, -7.897499167952783949, 17.65096039353565160 ) ) ;
#2129=CARTESIAN_POINT ( 'NONE',  ( 13.66253082644668027, -4.184297042924940868, 38.16530575332426167 ) ) ;
#2131=CARTESIAN_POINT ( 'NONE',  ( -13.86271395683116836, 3.458313116067174953, 31.43508225166169368 ) ) ;
#2146=CIRCLE ( 'NONE', #2967, 0.7499999999999997780 ) ;
#2152=CARTESIAN_POINT ( 'NONE',  ( 8.370005009003978813, 7.147500832047211539, 32.36596039353565857 ) ) ;
#2153=DIRECTION ( 'NONE',  ( -1.000000000000000000, 0.000000000000000000, 0.000000000000000000 ) ) ;
#2154=FACE_OUTER_BOUND ( 'NONE', #2481, .T. ) ;
#2157=FACE_BOUND ( 'NONE', #4313, .T. ) ;
#2158=ORIENTED_EDGE ( 'NONE', *, *, #2269, .F. ) ;
#2159=CARTESIAN_POINT ( 'NONE',  ( 14.28750500900398634, 0.2357416791107340981, 35.93971039353567676 ) ) ;
#2160=CARTESIAN_POINT ( 'NONE',  ( 18.74250500900397753, 8.320472107924325483E-07, 32.36596039353566567 ) ) ;
#2165=ORIENTED_EDGE ( 'NONE', *, *, #3906, .F. ) ;
#2167=ORIENTED_EDGE ( 'NONE', *, *, #280, .T. ) ;
#2175=CARTESIAN_POINT ( 'NONE',  ( -13.94802723912598097, 3.098790239948968850, 30.57065727641915132 ) ) ;
#2176=DIRECTION ( 'NONE',  ( -1.000000000000000000, 0.000000000000000000, 0.000000000000000000 ) ) ;
#2186=EDGE_CURVE ( 'NONE', #2774, #563, #4078, .T. ) ;
#2188=VERTEX_POINT ( 'NONE', #905 ) ;
#2190=EDGE_CURVE ( 'NONE', #919, #2774, #2284, .T. ) ;
#2192=EDGE_CURVE ( 'NONE', #3808, #2867, #1282, .T. ) ;
#2194=CARTESIAN_POINT ( 'NONE',  ( 13.83333314027810523, -3.573749167952788408, 32.36596039353566567 ) ) ;
#2196=CARTESIAN_POINT ( 'NONE',  ( -12.02323308010481107, 7.719129963227447710, 17.66658805193229753 ) ) ;
#2197=CARTESIAN_POINT ( 'NONE',  ( -12.87887028452541749, 6.192547044564507885, 35.96503381882250494 ) ) ;
#2199=CARTESIAN_POINT ( 'NONE',  ( 14.00291886944279973, -2.840536506667706629, 30.18479712748602140 ) ) ;
#2200=CARTESIAN_POINT ( 'NONE',  ( -13.83332312227014604, -3.573749167952787076, 32.13020424815260867 ) ) ;
#2202=CARTESIAN_POINT ( 'NONE',  ( 5.009003980371977336E-06, 8.320472128100606877E-07, 17.65096039353565160 ) ) ;
#2207=ORIENTED_EDGE ( 'NONE', *, *, #1799, .T. ) ;
#2208=CYLINDRICAL_SURFACE ( 'NONE', #1797, 0.7500000000000006661 ) ;
#2209=CARTESIAN_POINT ( 'NONE',  ( 6.870005009003977925, 12.08587093932537826, 18.40096039353565160 ) ) ;
#2211=ADVANCED_FACE ( 'NONE', ( #1246 ), #410, .T. ) ;
#2217=CYLINDRICAL_SURFACE ( 'NONE', #4271, 0.7499999999999997780 ) ;
#2218=CARTESIAN_POINT ( 'NONE',  ( -13.83332312227014249, -3.573749167952786632, 32.36596039353566567 ) ) ;
#2219=CARTESIAN_POINT ( 'NONE',  ( 3.750005009003979595, 8.320472128100606877E-07, 17.65096039353565160 ) ) ;
#2221=DIRECTION ( 'NONE',  ( -1.000000000000000000, 1.076498916035107744E-16, 0.000000000000000000 ) ) ;
#2224=FACE_OUTER_BOUND ( 'NONE', #1241, .T. ) ;
#2226=CIRCLE ( 'NONE', #352, 0.7499999999999997780 ) ;
#2231=FACE_OUTER_BOUND ( 'NONE', #3444, .T. ) ;
#2232=ORIENTED_EDGE ( 'NONE', *, *, #72, .F. ) ;
#2233=CARTESIAN_POINT ( 'NONE',  ( 12.37117714425454373, 7.897500832047208874, 17.65096039353565160 ) ) ;
#2234=ORIENTED_EDGE ( 'NONE', *, *, #4225, .F. ) ;
#2238=ORIENTED_EDGE ( 'NONE', *, *, #1349, .F. ) ;
#2240=CARTESIAN_POINT ( 'NONE',  ( -13.66252080843872108, 4.184298707019366681, 38.16530575332425457 ) ) ;
#2246=DIRECTION ( 'NONE',  ( -2.312964634635740689E-15, 0.000000000000000000, -1.000000000000000000 ) ) ;
#2256=CARTESIAN_POINT ( 'NONE',  ( -17.48249499099600968, -7.147499167952783061, 32.36596039353565857 ) ) ;
#2258=ADVANCED_FACE ( 'NONE', ( #246 ), #1111, .F. ) ;
#2260=VERTEX_POINT ( 'NONE', #4510 ) ;
#2263=DIRECTION ( 'NONE',  ( -1.000000000000000000, 0.000000000000000000, 0.000000000000000000 ) ) ;
#2264=ORIENTED_EDGE ( 'NONE', *, *, #3944, .T. ) ;
#2265=CARTESIAN_POINT ( 'NONE',  ( -12.39928141451404997, 7.099434970714632698, 33.31939447329315129 ) ) ;
#2269=EDGE_CURVE ( 'NONE', #719, #3403, #1221, .T. ) ;
#2272=CARTESIAN_POINT ( 'NONE',  ( -12.13298321006529790, 7.545450160427720654, 17.73224578507567628 ) ) ;
#2277=DIRECTION ( 'NONE',  ( 1.000000000000000000, 0.000000000000000000, 0.000000000000000000 ) ) ;
#2278=AXIS2_PLACEMENT_3D ( 'NONE', #70, #321, #1029 ) ;
#2280=DIRECTION ( 'NONE',  ( 0.000000000000000000, 0.000000000000000000, 1.000000000000000000 ) ) ;
#2284=LINE ( 'NONE', #197, #4029 ) ;
#2285=LINE ( 'NONE', #1989, #3477 ) ;
#2288=CARTESIAN_POINT ( 'NONE',  ( 14.99250500900397753, 8.320472111961197689E-07, 32.36596039353565857 ) ) ;
#2294=DIRECTION ( 'NONE',  ( 0.000000000000000000, 0.000000000000000000, -1.000000000000000000 ) ) ;
#2297=B_SPLINE_CURVE_WITH_KNOTS ( 'NONE', 3,
 ( #3190, #4534, #2831, #1051, #689, #80, #2942, #2199, #1853, #1503, #3676, #3213, #1078, #710, #1811, #3233, #1461, #1465 ),
 .UNSPECIFIED., .F., .F.,
 ( 4, 2, 2, 2, 2, 2, 2, 2, 4 ),
 ( 0.000000000000000000, 0.0007012932024186013802, 0.001402586404837202760, 0.002103879607255804141, 0.002805172809674405521, 0.003506466012093006901, 0.004207759214511608281, 0.004909052416930209661, 0.005610345619348811042 ),
 .UNSPECIFIED. ) ;
#2299=VERTEX_POINT ( 'NONE', #2934 ) ;
#2300=ORIENTED_EDGE ( 'NONE', *, *, #643, .T. ) ;
#2304=VERTEX_POINT ( 'NONE', #1019 ) ;
#2308=ADVANCED_FACE ( 'NONE', ( #795 ), #3515, .F. ) ;
#2310=CARTESIAN_POINT ( 'NONE',  ( 13.60392201806077495, 4.370505649930263914, 38.02622764783904330 ) ) ;
#2312=DIRECTION ( 'NONE',  ( 1.000000000000000000, -1.076498916035107621E-16, 0.000000000000000000 ) ) ;
#2314=AXIS2_PLACEMENT_3D ( 'NONE', #2288, #506, #3705 ) ;
#2316=DIRECTION ( 'NONE',  ( 1.000000000000000000, -8.673617379884035472E-17, 0.000000000000000000 ) ) ;
#2323=ORIENTED_EDGE ( 'NONE', *, *, #2122, .T. ) ;
#2324=CARTESIAN_POINT ( 'NONE',  ( -14.28749499099602005, 0.4808415968314561639, 39.51346039353565942 ) ) ;
#2325=CARTESIAN_POINT ( 'NONE',  ( 12.37117714425454551, -7.147499167952786614, 32.36596039353565857 ) ) ;
#2326=CIRCLE ( 'NONE', #2398, 0.7500000000000006661 ) ;
#2327=EDGE_CURVE ( 'NONE', #563, #1729, #2226, .T. ) ;
#2328=CIRCLE ( 'NONE', #4369, 7.147499999999999076 ) ;
#2329=EDGE_CURVE ( 'NONE', #2845, #2188, #422, .T. ) ;
#2333=DIRECTION ( 'NONE',  ( 0.000000000000000000, 0.000000000000000000, 1.000000000000000000 ) ) ;
#2335=CARTESIAN_POINT ( 'NONE',  ( 13.05598645602221808, 5.804670611569964223, 36.54283959188025221 ) ) ;
#2340=DIRECTION ( 'NONE',  ( 9.517981353260378315E-33, -8.841607930564763213E-17, 1.000000000000000000 ) ) ;
#2346=EDGE_CURVE ( 'NONE', #1947, #719, #3163, .T. ) ;
#2348=UNCERTAINTY_MEASURE_WITH_UNIT (LENGTH_MEASURE( 1.000000000000000082E-05 ), #740, 'distance_accuracy_value', 'NONE');
#2353=CARTESIAN_POINT ( 'NONE',  ( 14.19373587001559933, 1.650820511743084307, 39.32424842390233266 ) ) ;
#2355=CARTESIAN_POINT ( 'NONE',  ( -17.48249499099600968, -7.147499167952782173, 3.790960393535648176 ) ) ;
#2356=CARTESIAN_POINT ( 'NONE',  ( 13.94778095975370569, -3.099991964203534955, 34.15945326479446464 ) ) ;
#2363=VERTEX_POINT ( 'NONE', #2489 ) ;
#2364=VECTOR ( 'NONE', #1326, 1000.000000000000000 ) ;
#2365=CARTESIAN_POINT ( 'NONE',  ( 7.620005009003980589, -6.397499167952788390, 32.36596039353565857 ) ) ;
#2366=CARTESIAN_POINT ( 'NONE',  ( -14.28749499099602005, 8.320472128100606877E-07, 17.65096039353565160 ) ) ;
#2369=AXIS2_PLACEMENT_3D ( 'NONE', #1927, #4061, #4159 ) ;
#2371=VECTOR ( 'NONE', #1970, 1000.000000000000000 ) ;
#2373=CARTESIAN_POINT ( 'NONE',  ( 14.28750500900398279, 8.320472145597748469E-07, 28.79221039353566880 ) ) ;
#2376=CARTESIAN_POINT ( 'NONE',  ( -14.20052797712670767, -1.588767894053844554, 35.57559508471577914 ) ) ;
#2377=CIRCLE ( 'NONE', #213, 1.499999999999999556 ) ;
#2379=CARTESIAN_POINT ( 'NONE',  ( 14.09186599505832405, -2.362174669806939686, 35.05771999556577612 ) ) ;
#2384=CARTESIAN_POINT ( 'NONE',  ( 8.370005009003978813, 6.397500832047211539, 18.40096039353565160 ) ) ;
#2392=ORIENTED_EDGE ( 'NONE', *, *, #748, .T. ) ;
#2394=CARTESIAN_POINT ( 'NONE',  ( -13.93157463382742378, -3.199237769333737713, 38.77442139588517733 ) ) ;
#2396=DIRECTION ( 'NONE',  ( 0.000000000000000000, 0.000000000000000000, 1.000000000000000000 ) ) ;
#2398=AXIS2_PLACEMENT_3D ( 'NONE', #3168, #1510, #2925 ) ;
#2401=EDGE_CURVE ( 'NONE', #2299, #952, #2673, .T. ) ;
#2402=CARTESIAN_POINT ( 'NONE',  ( 13.88012347307862449, -3.388720364211946556, 33.52461916018275190 ) ) ;
#2407=VECTOR ( 'NONE', #3585, 1000.000000000000000 ) ;
#2408=CARTESIAN_POINT ( 'NONE',  ( 11.90639614989969886, 7.897500832047208874, 17.65096039353565160 ) ) ;
#2412=CARTESIAN_POINT ( 'NONE',  ( -13.83332312227014427, 3.573750832047213777, 32.36596039353566567 ) ) ;
#2417=ORIENTED_EDGE ( 'NONE', *, *, #743, .T. ) ;
#2422=CARTESIAN_POINT ( 'NONE',  ( 12.62992674139356097, -6.680416156580533560, 34.91794089097076892 ) ) ;
#2424=CARTESIAN_POINT ( 'NONE',  ( 14.17613779523199291, -1.791259416094247880, 35.46724785073431008 ) ) ;
#2425=CARTESIAN_POINT ( 'NONE',  ( -12.37116712624658454, 7.147500832047209762, 17.65096039353565160 ) ) ;
#2426=CARTESIAN_POINT ( 'NONE',  ( 8.370005009003978813, -7.147499167952784838, 17.65096039353565160 ) ) ;
#2428=ADVANCED_FACE ( 'NONE', ( #4096 ), #3365, .T. ) ;
#2435=CIRCLE ( 'NONE', #3870, 14.28750000000000142 ) ;
#2439=LINE ( 'NONE', #617, #579 ) ;
#2440=AXIS2_PLACEMENT_3D ( 'NONE', #1888, #288, #3560 ) ;
#2442=ORIENTED_EDGE ( 'NONE', *, *, #4127, .F. ) ;
#2443=CARTESIAN_POINT ( 'NONE',  ( 12.18303574196747263, 7.464156020238631228, 17.78097603577003127 ) ) ;
#2447=CARTESIAN_POINT ( 'NONE',  ( -13.83332312227014249, -3.573749167952786632, 32.36596039353566567 ) ) ;
#2448=CARTESIAN_POINT ( 'NONE',  ( 14.10222980048032326, -2.335234415017074294, 39.13740046776372594 ) ) ;
#2450=EDGE_CURVE ( 'NONE', #2014, #1208, #796, .T. ) ;
#2452=CARTESIAN_POINT ( 'NONE',  ( -12.27078712905513314, -7.318982076682964966, 17.91363472736961171 ) ) ;
#2453=CIRCLE ( 'NONE', #4343, 3.573749999999999538 ) ;
#2457=CARTESIAN_POINT ( 'NONE',  ( 18.74250500900397753, -3.573749167952788852, 32.36596039353566567 ) ) ;
#2459=CYLINDRICAL_SURFACE ( 'NONE', #1320, 3.573749999999999538 ) ;
#2464=VERTEX_POINT ( 'NONE', #3004 ) ;
#2465=CARTESIAN_POINT ( 'NONE',  ( 12.30672194145874876, 7.258094028239606921, 17.99507373849869651 ) ) ;
#2469=CARTESIAN_POINT ( 'NONE',  ( 8.370005009003978813, -7.897499167952783949, 17.65096039353565160 ) ) ;
#2470=CARTESIAN_POINT ( 'NONE',  ( 13.48425421428311211, -4.726822391962680392, 37.73224719609672917 ) ) ;
#2479=AXIS2_PLACEMENT_3D ( 'NONE', #3848, #1419, #629 ) ;
#2480=AXIS2_PLACEMENT_3D ( 'NONE', #3524, #296, #1744 ) ;
#2481=EDGE_LOOP ( 'NONE', ( #3602, #776, #379, #3416 ) ) ;
#2483=CIRCLE ( 'NONE', #4296, 0.7499999999999997780 ) ;
#2485=EDGE_LOOP ( 'NONE', ( #1761, #3065, #1662, #3771, #1538 ) ) ;
#2488=ORIENTED_EDGE ( 'NONE', *, *, #4005, .F. ) ;
#2489=CARTESIAN_POINT ( 'NONE',  ( 3.750005009003979595, -3.749999167952787538, 17.65096039353565160 ) ) ;
#2490=EDGE_LOOP ( 'NONE', ( #124, #4062, #1018, #2238 ) ) ;
#2491=CARTESIAN_POINT ( 'NONE',  ( 14.99250500900398109, 7.147500832047209762, 3.790960393535649064 ) ) ;
#2493=CARTESIAN_POINT ( 'NONE',  ( -13.05553858772694120, 5.805647905067521819, 36.54145662508980053 ) ) ;
#2502=CARTESIAN_POINT ( 'NONE',  ( 14.24247714116602737, 1.154283519900359600, 35.75635498855329786 ) ) ;
#2504=EDGE_CURVE ( 'NONE', #2506, #3737, #1420, .T. ) ;
#2506=VERTEX_POINT ( 'NONE', #4038 ) ;
#2510=EDGE_CURVE ( 'NONE', #1208, #2845, #1468, .T. ) ;
#2511=ORIENTED_EDGE ( 'NONE', *, *, #2122, .F. ) ;
#2516=LINE ( 'NONE', #4317, #3911 ) ;
#2518=CARTESIAN_POINT ( 'NONE',  ( -12.37116712624658810, -7.147499167952783061, 18.40096039353565160 ) ) ;
#2522=PLANE ( 'NONE',  #818 ) ;
#2527=DIRECTION ( 'NONE',  ( -1.000000000000000000, 8.673617379884035472E-17, 0.000000000000000000 ) ) ;
#2528=FACE_OUTER_BOUND ( 'NONE', #3649, .T. ) ;
#2534=ORIENTED_EDGE ( 'NONE', *, *, #2510, .T. ) ;
#2546=CARTESIAN_POINT ( 'NONE',  ( -12.37116712624658810, -7.147499167952783061, 18.40096039353565160 ) ) ;
#2547=DIRECTION ( 'NONE',  ( 1.000000000000000000, -1.076498916035107744E-16, 0.000000000000000000 ) ) ;
#2562=DIRECTION ( 'NONE',  ( 0.000000000000000000, -1.000000000000000000, 0.000000000000000000 ) ) ;
#2566=VERTEX_POINT ( 'NONE', #463 ) ;
#2567=ORIENTED_EDGE ( 'NONE', *, *, #1923, .T. ) ;
#2571=CARTESIAN_POINT ( 'NONE',  ( -13.87970016671034656, 3.390430244675832316, 31.21191674207121380 ) ) ;
#2589=ORIENTED_EDGE ( 'NONE', *, *, #2327, .T. ) ;
#2590=CARTESIAN_POINT ( 'NONE',  ( -14.17583154969198134, 1.793507453721278511, 35.46587530915064690 ) ) ;
#2592=DIRECTION ( 'NONE',  ( 0.000000000000000000, 0.000000000000000000, -1.000000000000000000 ) ) ;
#2598=DIRECTION ( 'NONE',  ( 1.076498916035107621E-16, -1.000000000000000000, 0.000000000000000000 ) ) ;
#2601=CARTESIAN_POINT ( 'NONE',  ( 13.92222260900385855, 3.211378106144403777, 33.95122015944071592 ) ) ;
#2605=ADVANCED_FACE ( 'NONE', ( #655, #2157 ), #206, .F. ) ;
#2606=DIRECTION ( 'NONE',  ( -1.000000000000000000, 1.076498916035107744E-16, 0.000000000000000000 ) ) ;
#2607=EDGE_LOOP ( 'NONE', ( #4326, #2300, #662, #2661 ) ) ;
#2611=ADVANCED_FACE ( 'NONE', ( #1629 ), #3045, .F. ) ;
#2614=CARTESIAN_POINT ( 'NONE',  ( 14.03228230178743097, 2.693715529912121820, 30.00579653744681252 ) ) ;
#2621=EDGE_CURVE ( 'NONE', #563, #2566, #2977, .T. ) ;
#2624=CARTESIAN_POINT ( 'NONE',  ( -12.18356977001436370, 7.463263818241263614, 17.78165220884836728 ) ) ;
#2625=DIRECTION ( 'NONE',  ( -1.076498916035107621E-16, -1.000000000000000000, -8.841607930564763213E-17 ) ) ;
#2629=ORIENTED_EDGE ( 'NONE', *, *, #643, .F. ) ;
#2630=DIRECTION ( 'NONE',  ( 0.000000000000000000, 0.000000000000000000, -1.000000000000000000 ) ) ;
#2661=ORIENTED_EDGE ( 'NONE', *, *, #3944, .F. ) ;
#2666=CARTESIAN_POINT ( 'NONE',  ( 13.30105870961065584, 5.219633490845899892, 37.25417504454090079 ) ) ;
#2669=VERTEX_POINT ( 'NONE', #2695 ) ;
#2670=DIRECTION ( 'NONE',  ( 0.000000000000000000, -1.000000000000000000, 0.000000000000000000 ) ) ;
#2671=ADVANCED_FACE ( 'NONE', ( #4466 ), #935, .T. ) ;
#2673=CIRCLE ( 'NONE', #4333, 1.499999999999999556 ) ;
#2675=LINE ( 'NONE', #1151, #1043 ) ;
#2683=ORIENTED_EDGE ( 'NONE', *, *, #4573, .T. ) ;
#2690=AXIS2_PLACEMENT_3D ( 'NONE', #2491, #708, #3934 ) ;
#2691=CARTESIAN_POINT ( 'NONE',  ( 6.870005009003979701, -6.397499167952786614, 17.65096039353565160 ) ) ;
#2695=CARTESIAN_POINT ( 'NONE',  ( 12.37117714425454551, 7.147500832047209762, 32.36596039353565857 ) ) ;
#2702=EDGE_LOOP ( 'NONE', ( #2034, #3530, #1123, #842, #584 ) ) ;
#2705=ORIENTED_EDGE ( 'NONE', *, *, #113, .F. ) ;
#2707=EDGE_LOOP ( 'NONE', ( #2323, #2392, #3078, #2937, #3977 ) ) ;
#2708=CARTESIAN_POINT ( 'NONE',  ( -12.37116712624658810, -7.147499167952783061, 32.36596039353565857 ) ) ;
#2716=CARTESIAN_POINT ( 'NONE',  ( 14.09723262389519149, 2.335210255262312184, 39.12537387803049427 ) ) ;
#2717=DIRECTION ( 'NONE',  ( -0.000000000000000000, -0.000000000000000000, -1.000000000000000000 ) ) ;
#2720=CARTESIAN_POINT ( 'NONE',  ( 7.620005009003978813, 3.573750832047212000, 32.36596039353566567 ) ) ;
#2729=EDGE_LOOP ( 'NONE', ( #310, #3034, #4146, #1804 ) ) ;
#2735=CARTESIAN_POINT ( 'NONE',  ( -12.50411890890981148, -6.913100685710334758, 34.24151272312386141 ) ) ;
#2736=CARTESIAN_POINT ( 'NONE',  ( 12.39929143252201271, -7.099433306620209549, 33.31939447329314419 ) ) ;
#2741=ORIENTED_EDGE ( 'NONE', *, *, #4635, .F. ) ;
#2756=CARTESIAN_POINT ( 'NONE',  ( -13.66281077095347207, -4.183336980462362575, 38.16598501014195932 ) ) ;
#2760=AXIS2_PLACEMENT_3D ( 'NONE', #4473, #2008, #3442 ) ;
#2765=DIRECTION ( 'NONE',  ( 1.000000000000000000, -1.076498916035107621E-16, 0.000000000000000000 ) ) ;
#2766=ORIENTED_EDGE ( 'NONE', *, *, #3033, .T. ) ;
#2767=LINE ( 'NONE', #631, #2906 ) ;
#2770=VERTEX_POINT ( 'NONE', #521 ) ;
#2773=VECTOR ( 'NONE', #276, 1000.000000000000000 ) ;
#2774=VERTEX_POINT ( 'NONE', #1965 ) ;
#2779=APPLICATION_CONTEXT ( 'automotive_design' ) ;
#2780=B_SPLINE_CURVE_WITH_KNOTS ( 'NONE', 3,
 ( #2030, #169, #1499, #1529, #4117, #4387, #2590, #4028, #803, #3739, #517, #1961, #544, #3417, #191, #4590, #1724, #2412 ),
 .UNSPECIFIED., .F., .F.,
 ( 4, 2, 2, 2, 2, 2, 2, 2, 4 ),
 ( 1.014071938996880503E-18, 0.0007013035162779028249, 0.001402607032555804783, 0.002103910548833706415, 0.002805214065111607830, 0.003506517581389509246, 0.004207821097667410228, 0.004909124613945311209, 0.005610428130223212191 ),
 .UNSPECIFIED. ) ;
#2781=CARTESIAN_POINT ( 'NONE',  ( 14.28750500900398279, 8.320472145597748469E-07, 3.790960393535649064 ) ) ;
#2782=CARTESIAN_POINT ( 'NONE',  ( -6.869994990996021400, -6.397499167952784838, 17.65096039353565160 ) ) ;
#2792=FACE_OUTER_BOUND ( 'NONE', #2079, .T. ) ;
#2793=VERTEX_POINT ( 'NONE', #3670 ) ;
#2801=CARTESIAN_POINT ( 'NONE',  ( 12.13220478356813636, 7.546708218815218139, 17.73167833386938597 ) ) ;
#2805=DIRECTION ( 'NONE',  ( 1.000000000000000000, 1.076498916035107621E-16, -0.000000000000000000 ) ) ;
#2809=CARTESIAN_POINT ( 'NONE',  ( 13.83333314027810523, -3.573749167952788408, 32.36596039353566567 ) ) ;
#2819=ORIENTED_EDGE ( 'NONE', *, *, #123, .F. ) ;
#2824=AXIS2_PLACEMENT_3D ( 'NONE', #1960, #3389, #820 ) ;
#2825=PRODUCT ( 'Part 130_Varsay\X2\0131\X0\lan', 'Part 130_Varsay\X2\0131\X0\lan', '', ( #1075 ) ) ;
#2826=EDGE_LOOP ( 'NONE', ( #417, #50, #1531, #4217, #53, #396, #2167, #1084, #2056, #3762, #511, #4629 ) ) ;
#2828=VERTEX_POINT ( 'NONE', #565 ) ;
#2831=CARTESIAN_POINT ( 'NONE',  ( 13.83943268946890193, -3.550368327121672163, 31.89570794180626123 ) ) ;
#2835=CIRCLE ( 'NONE', #1425, 7.147499999999999076 ) ;
#2838=ORIENTED_EDGE ( 'NONE', *, *, #1582, .T. ) ;
#2843=ORIENTED_EDGE ( 'NONE', *, *, #265, .T. ) ;
#2845=VERTEX_POINT ( 'NONE', #924 ) ;
#2846=CARTESIAN_POINT ( 'NONE',  ( 14.99250500900398109, 7.897500832047208874, 18.40096039353565160 ) ) ;
#2851=AXIS2_PLACEMENT_3D ( 'NONE', #3290, #693, #2153 ) ;
#2853=CARTESIAN_POINT ( 'NONE',  ( -14.03269742075053195, 2.691508642874120394, 30.00328177004153574 ) ) ;
#2855=EDGE_CURVE ( 'NONE', #3260, #4527, #2055, .T. ) ;
#2858=DIRECTION ( 'NONE',  ( 1.000000000000000000, 0.000000000000000000, 0.000000000000000000 ) ) ;
#2860=ADVANCED_FACE ( 'NONE', ( #656 ), #3812, .F. ) ;
#2867=VERTEX_POINT ( 'NONE', #3492 ) ;
#2871=CARTESIAN_POINT ( 'NONE',  ( -3.749994990996019517, 3.750000832047212906, 3.790960393535649064 ) ) ;
#2872=DIRECTION ( 'NONE',  ( 1.000000000000000000, 0.000000000000000000, 0.000000000000000000 ) ) ;
#2874=DIRECTION ( 'NONE',  ( -0.000000000000000000, -0.000000000000000000, -1.000000000000000000 ) ) ;
#2875=CARTESIAN_POINT ( 'NONE',  ( -14.12120469946661494, -2.182301628983542852, 29.52629215715650091 ) ) ;
#2876=CARTESIAN_POINT ( 'NONE',  ( 5.009003980371977336E-06, 3.750000832047212906, 18.79096039353565217 ) ) ;
#2878=FACE_BOUND ( 'NONE', #4444, .T. ) ;
#2880=SURFACE_STYLE_FILL_AREA ( #393 ) ;
#2882=ORIENTED_EDGE ( 'NONE', *, *, #659, .T. ) ;
#2883=DIRECTION ( 'NONE',  ( 0.000000000000000000, 1.000000000000000000, 0.000000000000000000 ) ) ;
#2885=ORIENTED_EDGE ( 'NONE', *, *, #2076, .T. ) ;
#2889=ORIENTED_EDGE ( 'NONE', *, *, #2329, .F. ) ;
#2891=( GEOMETRIC_REPRESENTATION_CONTEXT ( 3 ) GLOBAL_UNCERTAINTY_ASSIGNED_CONTEXT ( ( #569 ) ) GLOBAL_UNIT_ASSIGNED_CONTEXT ( ( #2969, #504, #3776 ) ) REPRESENTATION_CONTEXT ( 'NONE', 'WORKASPACE' ) );
#2897=ADVANCED_FACE ( 'NONE', ( #2792 ), #799, .T. ) ;
#2898=CARTESIAN_POINT ( 'NONE',  ( -13.92247150553487600, 3.210277310620725633, 30.77820937948456503 ) ) ;
#2899=CARTESIAN_POINT ( 'NONE',  ( 5.009003980371977336E-06, 8.320472128100606877E-07, 17.65096039353565160 ) ) ;
#2901=CARTESIAN_POINT ( 'NONE',  ( 7.620005009003977037, 6.397500832047211539, 32.36596039353565857 ) ) ;
#2903=EDGE_LOOP ( 'NONE', ( #3321, #2683, #3206, #1477 ) ) ;
#2904=FACE_OUTER_BOUND ( 'NONE', #2826, .T. ) ;
#2906=VECTOR ( 'NONE', #3900, 1000.000000000000000 ) ;
#2913=EDGE_LOOP ( 'NONE', ( #1441, #3995 ) ) ;
#2916=CARTESIAN_POINT ( 'NONE',  ( 14.28750500900397746, 0.2341033329457500312, 28.79221039353566525 ) ) ;
#2918=DIRECTION ( 'NONE',  ( -1.000000000000000000, 1.076498916035107621E-16, -0.000000000000000000 ) ) ;
#2921=CYLINDRICAL_SURFACE ( 'NONE', #4178, 14.28750000000000142 ) ;
#2925=DIRECTION ( 'NONE',  ( 1.000000000000000000, 0.000000000000000000, 0.000000000000000000 ) ) ;
#2930=CARTESIAN_POINT ( 'NONE',  ( 14.12152177866159874, 2.180236281663612719, 35.20712478225889441 ) ) ;
#2932=VECTOR ( 'NONE', #1239, 1000.000000000000000 ) ;
#2934=CARTESIAN_POINT ( 'NONE',  ( -8.369994990996019624, -7.897499167952782173, 17.65096039353565160 ) ) ;
#2935=DIRECTION ( 'NONE',  ( 1.000000000000000000, 0.000000000000000000, 0.000000000000000000 ) ) ;
#2937=ORIENTED_EDGE ( 'NONE', *, *, #3937, .F. ) ;
#2939=DIRECTION ( 'NONE',  ( 0.000000000000000000, 0.000000000000000000, 1.000000000000000000 ) ) ;
#2941=SHAPE_DEFINITION_REPRESENTATION ( #2118, #1005 ) ;
#2942=CARTESIAN_POINT ( 'NONE',  ( 13.94776995008254694, -3.100015636283709242, 30.57263291037062203 ) ) ;
#2949=AXIS2_PLACEMENT_3D ( 'NONE', #1117, #3179, #1842 ) ;
#2951=ORIENTED_EDGE ( 'NONE', *, *, #2450, .F. ) ;
#2952=FACE_OUTER_BOUND ( 'NONE', #2490, .T. ) ;
#2958=CARTESIAN_POINT ( 'NONE',  ( -12.37116712624658099, 7.147500832047212427, 18.40096039353565160 ) ) ;
#2961=ORIENTED_EDGE ( 'NONE', *, *, #36, .F. ) ;
#2967=AXIS2_PLACEMENT_3D ( 'NONE', #1635, #38, #1483 ) ;
#2969=( LENGTH_UNIT ( ) NAMED_UNIT ( * ) SI_UNIT ( .MILLI., .METRE. ) );
#2977=CIRCLE ( 'NONE', #2369, 6.397499999999999964 ) ;
#2978=CARTESIAN_POINT ( 'NONE',  ( 5.009003980371977336E-06, 8.320472128100606877E-07, 3.790960393535649064 ) ) ;
#2979=DIRECTION ( 'NONE',  ( 0.000000000000000000, -1.000000000000000000, 0.000000000000000000 ) ) ;
#2984=AXIS2_PLACEMENT_3D ( 'NONE', #2384, #3490, #3531 ) ;
#2985=DIRECTION ( 'NONE',  ( -1.000000000000000000, 1.076498916035107744E-16, -0.000000000000000000 ) ) ;
#2988=CARTESIAN_POINT ( 'NONE',  ( 14.09176629432668015, 2.362873823246649962, 29.67462178077400736 ) ) ;
#2989=CARTESIAN_POINT ( 'NONE',  ( -13.83332312227014249, -3.573749167952786632, 32.36596039353566567 ) ) ;
#2991=CARTESIAN_POINT ( 'NONE',  ( -12.37116712624657922, 7.147500832047210650, 32.84705871297352076 ) ) ;
#2994=VECTOR ( 'NONE', #599, 1000.000000000000000 ) ;
#3004=CARTESIAN_POINT ( 'NONE',  ( -7.619994990996019624, -3.573749167952786188, 32.36596039353566567 ) ) ;
#3007=DIRECTION ( 'NONE',  ( -1.076498916035107621E-16, -1.000000000000000000, 0.000000000000000000 ) ) ;
#3008=CIRCLE ( 'NONE', #3767, 3.573749999999999538 ) ;
#3013=CARTESIAN_POINT ( 'NONE',  ( -8.369994990996019624, -7.147499167952784838, 32.36596039353565857 ) ) ;
#3014=ORIENTED_EDGE ( 'NONE', *, *, #3150, .F. ) ;
#3015=ADVANCED_FACE ( 'NONE', ( #3974 ), #2459, .F. ) ;
#3019=CARTESIAN_POINT ( 'NONE',  ( 8.370005009003978813, 7.897500832047212427, 17.65096039353565160 ) ) ;
#3026=DIRECTION ( 'NONE',  ( 0.000000000000000000, -1.000000000000000000, 0.000000000000000000 ) ) ;
#3033=EDGE_CURVE ( 'NONE', #1779, #4527, #4615, .T. ) ;
#3034=ORIENTED_EDGE ( 'NONE', *, *, #1934, .T. ) ;
#3036=CARTESIAN_POINT ( 'NONE',  ( 14.12133832020656676, 2.181416654277627654, 29.52570525180092176 ) ) ;
#3045=PLANE ( 'NONE',  #3055 ) ;
#3050=FACE_OUTER_BOUND ( 'NONE', #2485, .T. ) ;
#3051=EDGE_LOOP ( 'NONE', ( #2838, #3561, #2264, #1189, #1801 ) ) ;
#3053=VECTOR ( 'NONE', #3668, 1000.000000000000000 ) ;
#3055=AXIS2_PLACEMENT_3D ( 'NONE', #1228, #3073, #3729 ) ;
#3059=VERTEX_POINT ( 'NONE', #1755 ) ;
#3062=CARTESIAN_POINT ( 'NONE',  ( -14.10221978247235874, 2.335236079111500995, 39.13740046776371884 ) ) ;
#3065=ORIENTED_EDGE ( 'NONE', *, *, #36, .T. ) ;
#3071=CARTESIAN_POINT ( 'NONE',  ( 13.93158465183538475, 3.199239433428168411, 38.77442139588518444 ) ) ;
#3073=DIRECTION ( 'NONE',  ( -8.673617379884035472E-17, -1.000000000000000000, 0.000000000000000000 ) ) ;
#3075=ORIENTED_EDGE ( 'NONE', *, *, #3866, .T. ) ;
#3076=AXIS2_PLACEMENT_3D ( 'NONE', #1413, #959, #4535 ) ;
#3078=ORIENTED_EDGE ( 'NONE', *, *, #3488, .T. ) ;
#3081=ORIENTED_EDGE ( 'NONE', *, *, #2621, .F. ) ;
#3085=EDGE_LOOP ( 'NONE', ( #73, #2417, #3926, #4236 ) ) ;
#3092=VECTOR ( 'NONE', #2918, 1000.000000000000000 ) ;
#3094=CARTESIAN_POINT ( 'NONE',  ( -14.00282433085553535, -2.840975162856891778, 34.54665773754472013 ) ) ;
#3097=AXIS2_PLACEMENT_3D ( 'NONE', #2209, #3641, #420 ) ;
#3098=ADVANCED_FACE ( 'NONE', ( #1234 ), #4233, .F. ) ;
#3099=CARTESIAN_POINT ( 'NONE',  ( -14.28749499099602005, 8.320472128100571937E-07, 28.79221039353566880 ) ) ;
#3100=ORIENTED_EDGE ( 'NONE', *, *, #4230, .F. ) ;
#3104=CARTESIAN_POINT ( 'NONE',  ( -12.62991672338559468, 6.680417820674964702, 34.91794089097075471 ) ) ;
#3108=ADVANCED_FACE ( 'NONE', ( #2231 ), #4400, .T. ) ;
#3109=AXIS2_PLACEMENT_3D ( 'NONE', #1958, #2606, #3026 ) ;
#3113=ORIENTED_EDGE ( 'NONE', *, *, #4114, .F. ) ;
#3116=EDGE_CURVE ( 'NONE', #3620, #2845, #1086, .T. ) ;
#3120=CARTESIAN_POINT ( 'NONE',  ( -14.28749499099602360, -0.2370289631965043498, 35.93971039353566965 ) ) ;
#3123=CARTESIAN_POINT ( 'NONE',  ( 14.25924429792894088, -0.9271090578520909675, 35.82528087157432140 ) ) ;
#3126=DIRECTION ( 'NONE',  ( -9.517981353260378315E-33, 8.841607930564763213E-17, -1.000000000000000000 ) ) ;
#3128=ORIENTED_EDGE ( 'NONE', *, *, #4230, .T. ) ;
#3129=AXIS2_PLACEMENT_3D ( 'NONE', #2899, #4342, #3289 ) ;
#3134=VECTOR ( 'NONE', #4503, 1000.000000000000000 ) ;
#3137=DIRECTION ( 'NONE',  ( -1.076498916035107621E-16, -1.000000000000000000, 0.000000000000000000 ) ) ;
#3139=CARTESIAN_POINT ( 'NONE',  ( -13.94746284641590428, -3.101372177908327199, 34.15706925759410950 ) ) ;
#3140=VECTOR ( 'NONE', #2527, 1000.000000000000000 ) ;
#3141=CARTESIAN_POINT ( 'NONE',  ( -8.369994990996016071, 6.397500832047212427, 3.790960393535649064 ) ) ;
#3148=AXIS2_PLACEMENT_3D ( 'NONE', #4554, #2805, #1764 ) ;
#3150=EDGE_CURVE ( 'NONE', #3903, #1497, #1695, .T. ) ;
#3152=EDGE_CURVE ( 'NONE', #2793, #3946, #3786, .T. ) ;
#3153=CARTESIAN_POINT ( 'NONE',  ( -14.28749499099602005, 8.320472128100606877E-07, 17.65096039353565160 ) ) ;
#3163=LINE ( 'NONE', #2233, #3053 ) ;
#3166=PLANE ( 'NONE',  #3148 ) ;
#3168=CARTESIAN_POINT ( 'NONE',  ( 8.370005009003978813, 6.397500832047211539, 32.36596039353565857 ) ) ;
#3179=DIRECTION ( 'NONE',  ( 0.000000000000000000, 0.000000000000000000, 1.000000000000000000 ) ) ;
#3182=B_SPLINE_CURVE_WITH_KNOTS ( 'NONE', 3,
 ( #3099, #4536, #1325, #602, #3483, #2875, #1054, #1415, #3235, #3215, #322, #411, #4368, #691, #2200, #2218 ),
 .UNSPECIFIED., .F., .F.,
 ( 4, 2, 2, 2, 2, 2, 2, 4 ),
 ( 0.01121786453620354437, 0.01261999568898470973, 0.01332106126537529155, 0.01402212684176587336, 0.01472319241815645517, 0.01542425799454703872, 0.01612532357093762053, 0.01682638914732820234 ),
 .UNSPECIFIED. ) ;
#3185=CARTESIAN_POINT ( 'NONE',  ( -8.369994990996016071, 6.397500832047212427, 32.36596039353565857 ) ) ;
#3189=CARTESIAN_POINT ( 'NONE',  ( -14.09151425697337778, -2.364203556260324302, 35.05593777286575374 ) ) ;
#3190=CARTESIAN_POINT ( 'NONE',  ( 13.83333314027810523, -3.573749167952788408, 32.36596039353566567 ) ) ;
#3195=CARTESIAN_POINT ( 'NONE',  ( 18.74250500900397753, -3.573749167952788852, 32.36596039353566567 ) ) ;
#3197=CARTESIAN_POINT ( 'NONE',  ( -3.749994990996019961, -3.749999167952787094, 17.65096039353565160 ) ) ;
#3199=CARTESIAN_POINT ( 'NONE',  ( -12.37116712624658454, 7.147500832047209762, 18.40096039353565160 ) ) ;
#3204=ORIENTED_EDGE ( 'NONE', *, *, #166, .T. ) ;
#3206=ORIENTED_EDGE ( 'NONE', *, *, #3857, .F. ) ;
#3209=PLANE ( 'NONE',  #2690 ) ;
#3213=CARTESIAN_POINT ( 'NONE',  ( 14.17609192062688095, -1.791678206414217156, 29.26486561848145840 ) ) ;
#3215=CARTESIAN_POINT ( 'NONE',  ( -13.94784893415634031, -3.099588501034327148, 30.57203322479964669 ) ) ;
#3217=VECTOR ( 'NONE', #3711, 1000.000000000000000 ) ;
#3221=CARTESIAN_POINT ( 'NONE',  ( 14.25909138040731605, 0.9292885604723594151, 35.82465120474719811 ) ) ;
#3233=CARTESIAN_POINT ( 'NONE',  ( 14.28174855069001303, -0.4668339671081180309, 28.81501425372158209 ) ) ;
#3235=CARTESIAN_POINT ( 'NONE',  ( -14.00274155455516478, -2.841332011922032663, 30.18594746002730744 ) ) ;
#3236=FACE_OUTER_BOUND ( 'NONE', #3339, .T. ) ;
#3243=CARTESIAN_POINT ( 'NONE',  ( 12.35746567010111185, -7.171350607572557045, 18.18649461234914710 ) ) ;
#3244=EDGE_CURVE ( 'NONE', #4361, #3620, #3915, .T. ) ;
#3252=VERTEX_POINT ( 'NONE', #2518 ) ;
#3256=EDGE_CURVE ( 'NONE', #1617, #3903, #4144, .T. ) ;
#3260=VERTEX_POINT ( 'NONE', #272 ) ;
#3267=CYLINDRICAL_SURFACE ( 'NONE', #2851, 0.7499999999999997780 ) ;
#3270=CARTESIAN_POINT ( 'NONE',  ( 12.27095706366207040, -7.318709742180212530, 17.91402383463540104 ) ) ;
#3271=ORIENTED_EDGE ( 'NONE', *, *, #375, .T. ) ;
#3273=DIRECTION ( 'NONE',  ( -1.000000000000000000, 1.076498916035107744E-16, 0.000000000000000000 ) ) ;
#3278=CLOSED_SHELL ( 'NONE', ( #3015, #2860, #4574, #4546, #2605, #1742, #4089, #1495, #1726, #2211, #3801, #3108, #2671, #2428, #1016, #4258, #925, #1454, #3595, #2258, #3874, #808, #3098, #4054, #1009, #2897, #1070, #3636, #3522, #1099, #1802, #2308, #4626, #1596, #2611, #4149 ) ) ;
#3282=DIRECTION ( 'NONE',  ( -0.000000000000000000, -0.000000000000000000, -1.000000000000000000 ) ) ;
#3289=DIRECTION ( 'NONE',  ( -1.000000000000000000, 0.000000000000000000, 0.000000000000000000 ) ) ;
#3290=CARTESIAN_POINT ( 'NONE',  ( 8.370005009003978813, 6.397500832047211539, 3.790960393535649064 ) ) ;
#3296=DIRECTION ( 'NONE',  ( 9.517981353260378315E-33, -8.841607930564763213E-17, 1.000000000000000000 ) ) ;
#3300=ORIENTED_EDGE ( 'NONE', *, *, #3945, .T. ) ;
#3304=ORIENTED_EDGE ( 'NONE', *, *, #2051, .T. ) ;
#3310=AXIS2_PLACEMENT_3D ( 'NONE', #1515, #3296, #746 ) ;
#3319=EDGE_CURVE ( 'NONE', #3535, #3784, #4247, .T. ) ;
#3321=ORIENTED_EDGE ( 'NONE', *, *, #1091, .T. ) ;
#3329=CARTESIAN_POINT ( 'NONE',  ( -13.30083885052560788, 5.220168816630788022, 37.25360547957401280 ) ) ;
#3333=CARTESIAN_POINT ( 'NONE',  ( -6.869994990996018736, 6.397500832047212427, 18.40096039353565160 ) ) ;
#3336=CARTESIAN_POINT ( 'NONE',  ( -12.37116712624658454, 7.147500832047209762, 18.40096039353565160 ) ) ;
#3339=EDGE_LOOP ( 'NONE', ( #1906, #2037, #3075, #1071 ) ) ;
#3351=AXIS2_PLACEMENT_3D ( 'NONE', #2876, #104, #554 ) ;
#3353=EDGE_CURVE ( 'NONE', #3260, #209, #3182, .T. ) ;
#3360=DIRECTION ( 'NONE',  ( -0.000000000000000000, -0.000000000000000000, -1.000000000000000000 ) ) ;
#3365=PLANE ( 'NONE',  #2824 ) ;
#3366=EDGE_CURVE ( 'NONE', #1488, #3260, #1895, .T. ) ;
#3367=AXIS2_PLACEMENT_3D ( 'NONE', #4092, #3412, #2670 ) ;
#3374=EDGE_CURVE ( 'NONE', #3946, #4385, #1222, .T. ) ;
#3376=ORIENTED_EDGE ( 'NONE', *, *, #527, .F. ) ;
#3379=CARTESIAN_POINT ( 'NONE',  ( -8.369994990996012518, 7.147500832047212427, 32.36596039353565857 ) ) ;
#3380=CARTESIAN_POINT ( 'NONE',  ( 12.50412892691776712, 6.913102349804759683, 34.24151272312386141 ) ) ;
#3382=ORIENTED_EDGE ( 'NONE', *, *, #4295, .F. ) ;
#3385=CARTESIAN_POINT ( 'NONE',  ( -3.749994990996019517, 3.750000832047212906, 3.790960393535649064 ) ) ;
#3389=DIRECTION ( 'NONE',  ( -1.076498916035107621E-16, -1.000000000000000000, -8.841607930564763213E-17 ) ) ;
#3398=EDGE_LOOP ( 'NONE', ( #3271, #4026, #823, #4241 ) ) ;
#3400=CARTESIAN_POINT ( 'NONE',  ( 14.00286243054562085, 2.840792968600885704, 30.18522767438163967 ) ) ;
#3403=VERTEX_POINT ( 'NONE', #1831 ) ;
#3405=DIRECTION ( 'NONE',  ( 0.000000000000000000, 1.000000000000000000, -0.000000000000000000 ) ) ;
#3411=VERTEX_POINT ( 'NONE', #4298 ) ;
#3412=DIRECTION ( 'NONE',  ( -1.000000000000000000, 1.076498916035107744E-16, 0.000000000000000000 ) ) ;
#3416=ORIENTED_EDGE ( 'NONE', *, *, #747, .F. ) ;
#3417=CARTESIAN_POINT ( 'NONE',  ( -13.87981781320283226, 3.389924195623678305, 33.52105921454751325 ) ) ;
#3418=CARTESIAN_POINT ( 'NONE',  ( -12.37116712624658454, -7.897499167952782173, 17.65096039353565160 ) ) ;
#3423=DIRECTION ( 'NONE',  ( -9.517981353260378315E-33, -8.841607930564763213E-17, 1.000000000000000000 ) ) ;
#3427=DIRECTION ( 'NONE',  ( -1.000000000000000000, 1.076498916035107621E-16, 0.000000000000000000 ) ) ;
#3437=ORIENTED_EDGE ( 'NONE', *, *, #2504, .T. ) ;
#3440=B_SPLINE_CURVE_WITH_KNOTS ( 'NONE', 3,
 ( #3499, #3546, #3914, #3844, #2448, #4580, #270, #2129, #598, #2470, #1323, #2043, #4176, #3863, #1785, #1697, #1366, #2422, #293, #1740, #623, #2736, #4269, #1717 ),
 .UNSPECIFIED., .F., .F.,
 ( 4, 2, 2, 2, 2, 2, 2, 2, 2, 2, 2, 4 ),
 ( 0.01136174788562026999, 0.01278160237203085359, 0.01420145685844143545, 0.01562131134485201904, 0.01633123858805730563, 0.01704116583126259049, 0.01775109307446787882, 0.01846102031767316368, 0.01988087480408372298, 0.02059080204728900437, 0.02130072929049427882, 0.02272058377690481731 ),
 .UNSPECIFIED. ) ;
#3441=ORIENTED_EDGE ( 'NONE', *, *, #1836, .T. ) ;
#3442=DIRECTION ( 'NONE',  ( 0.000000000000000000, 0.000000000000000000, 1.000000000000000000 ) ) ;
#3444=EDGE_LOOP ( 'NONE', ( #1691, #1474, #1173, #3882, #752 ) ) ;
#3447=DIRECTION ( 'NONE',  ( 1.000000000000000000, 0.000000000000000000, 0.000000000000000000 ) ) ;
#3455=CARTESIAN_POINT ( 'NONE',  ( -13.86245963902841716, -3.459327043890196407, 33.29303758927057544 ) ) ;
#3462=LINE ( 'NONE', #3195, #2364 ) ;
#3468=B_SPLINE_CURVE_WITH_KNOTS ( 'NONE', 3,
 ( #2447, #3545, #575, #3455, #3479, #248, #3139, #3094, #4533, #3189, #1322, #269, #2376, #4268, #3862, #3821, #3120, #3498 ),
 .UNSPECIFIED., .F., .F.,
 ( 4, 2, 2, 2, 2, 2, 2, 2, 4 ),
 ( 0.01682638914732820234, 0.01752717873359113318, 0.01822796831985406055, 0.01892875790611699138, 0.01962954749237991875, 0.02033033707864284959, 0.02103112666490578042, 0.02173191625116870779, 0.02243270583743163862 ),
 .UNSPECIFIED. ) ;
#3477=VECTOR ( 'NONE', #2263, 1000.000000000000000 ) ;
#3479=CARTESIAN_POINT ( 'NONE',  ( -13.87980917377075585, -3.389965183367340096, 33.52105365422744399 ) ) ;
#3480=DIRECTION ( 'NONE',  ( 1.000000000000000000, 0.000000000000000000, 0.000000000000000000 ) ) ;
#3482=VECTOR ( 'NONE', #1660, 1000.000000000000000 ) ;
#3483=CARTESIAN_POINT ( 'NONE',  ( -14.17571295649602980, -1.794442765457400224, 29.26658434350617810 ) ) ;
#3485=EDGE_LOOP ( 'NONE', ( #2705, #1584, #1598, #1845 ) ) ;
#3487=CIRCLE ( 'NONE', #1832, 14.28750000000000142 ) ;
#3488=EDGE_CURVE ( 'NONE', #4203, #195, #3008, .T. ) ;
#3490=DIRECTION ( 'NONE',  ( 0.000000000000000000, 0.000000000000000000, 1.000000000000000000 ) ) ;
#3492=CARTESIAN_POINT ( 'NONE',  ( -12.37116712624657033, 7.147500832047212427, 32.36596039353565857 ) ) ;
#3498=CARTESIAN_POINT ( 'NONE',  ( -14.28749499099602005, 8.320472117659611842E-07, 35.93971039353566255 ) ) ;
#3499=CARTESIAN_POINT ( 'NONE',  ( 14.28750500900398279, 8.320472145597748469E-07, 39.51346039353565942 ) ) ;
#3501=EDGE_CURVE ( 'NONE', #1729, #2867, #781, .T. ) ;
#3502=CARTESIAN_POINT ( 'NONE',  ( 14.00316917680643947, -2.839330532674458674, 34.54879557223570430 ) ) ;
#3504=ORIENTED_EDGE ( 'NONE', *, *, #1240, .T. ) ;
#3506=DIRECTION ( 'NONE',  ( 0.000000000000000000, -1.000000000000000000, 0.000000000000000000 ) ) ;
#3515=CYLINDRICAL_SURFACE ( 'NONE', #4488, 0.7500000000000006661 ) ;
#3520=CARTESIAN_POINT ( 'NONE',  ( 14.28750500900398279, 8.320472145597748469E-07, 39.51346039353565942 ) ) ;
#3522=ADVANCED_FACE ( 'NONE', ( #1573 ), #4213, .F. ) ;
#3524=CARTESIAN_POINT ( 'NONE',  ( 8.370005009003978813, -6.397499167952787502, 32.36596039353565857 ) ) ;
#3526=CARTESIAN_POINT ( 'NONE',  ( -8.369994990996016071, 7.147500832047212427, 18.40096039353565160 ) ) ;
#3529=AXIS2_PLACEMENT_3D ( 'NONE', #1273, #4512, #1924 ) ;
#3530=ORIENTED_EDGE ( 'NONE', *, *, #4074, .T. ) ;
#3531=DIRECTION ( 'NONE',  ( 1.000000000000000000, 0.000000000000000000, 0.000000000000000000 ) ) ;
#3533=DIRECTION ( 'NONE',  ( 0.000000000000000000, -1.000000000000000000, 0.000000000000000000 ) ) ;
#3535=VERTEX_POINT ( 'NONE', #247 ) ;
#3545=CARTESIAN_POINT ( 'NONE',  ( -13.83332312227014604, -3.573749167952787076, 32.60162372824473209 ) ) ;
#3546=CARTESIAN_POINT ( 'NONE',  ( 14.28750500900398279, -0.4808399327370302956, 39.51346039353565942 ) ) ;
#3550=CARTESIAN_POINT ( 'NONE',  ( -12.18302572395950989, -7.464154356144206304, 17.78097603577003127 ) ) ;
#3557=ORIENTED_EDGE ( 'NONE', *, *, #3866, .F. ) ;
#3560=DIRECTION ( 'NONE',  ( 1.000000000000000000, 0.000000000000000000, 0.000000000000000000 ) ) ;
#3561=ORIENTED_EDGE ( 'NONE', *, *, #4127, .T. ) ;
#3567=CARTESIAN_POINT ( 'NONE',  ( -14.17567608032355686, 1.794650183413384115, 29.26677597323998725 ) ) ;
#3572=CARTESIAN_POINT ( 'NONE',  ( 8.370005009003978813, 8.320472119090310841E-07, 32.36596039353565857 ) ) ;
#3576=ORIENTED_EDGE ( 'NONE', *, *, #3835, .F. ) ;
#3585=DIRECTION ( 'NONE',  ( 0.000000000000000000, 1.000000000000000000, 0.000000000000000000 ) ) ;
#3589=CARTESIAN_POINT ( 'NONE',  ( -12.35763252401195800, -7.171051608339699790, 18.18681329310062367 ) ) ;
#3590=VECTOR ( 'NONE', #3360, 1000.000000000000000 ) ;
#3591=CARTESIAN_POINT ( 'NONE',  ( 5.009003980371977336E-06, 8.320472128100606877E-07, 3.790960393535649064 ) ) ;
#3595=ADVANCED_FACE ( 'NONE', ( #2063 ), #514, .T. ) ;
#3602=ORIENTED_EDGE ( 'NONE', *, *, #2080, .F. ) ;
#3608=CARTESIAN_POINT ( 'NONE',  ( 3.750005009003979595, 3.750000832047212906, 17.65096039353565160 ) ) ;
#3611=CARTESIAN_POINT ( 'NONE',  ( 8.370005009003978813, -6.397499167952786614, 17.65096039353565160 ) ) ;
#3613=CARTESIAN_POINT ( 'NONE',  ( -12.37116712624659343, -7.147499167952783061, 18.29228486772271722 ) ) ;
#3614=FACE_OUTER_BOUND ( 'NONE', #4526, .T. ) ;
#3620=VERTEX_POINT ( 'NONE', #2691 ) ;
#3621=DIRECTION ( 'NONE',  ( -0.000000000000000000, -0.000000000000000000, -1.000000000000000000 ) ) ;
#3624=ORIENTED_EDGE ( 'NONE', *, *, #4635, .T. ) ;
#3629=ORIENTED_EDGE ( 'NONE', *, *, #2192, .T. ) ;
#3633=DIRECTION ( 'NONE',  ( -1.000000000000000000, -0.000000000000000000, -0.000000000000000000 ) ) ;
#3635=CARTESIAN_POINT ( 'NONE',  ( -13.83332312227014427, 3.573750832047213777, 32.36596039353566567 ) ) ;
#3636=ADVANCED_FACE ( 'NONE', ( #4219 ), #3861, .F. ) ;
#3640=FACE_BOUND ( 'NONE', #3485, .T. ) ;
#3641=DIRECTION ( 'NONE',  ( 1.076498916035107621E-16, -1.000000000000000000, 0.000000000000000000 ) ) ;
#3643=ORIENTED_EDGE ( 'NONE', *, *, #3353, .F. ) ;
#3649=EDGE_LOOP ( 'NONE', ( #2033, #4436, #2951, #2234 ) ) ;
#3655=DIRECTION ( 'NONE',  ( 1.076498916035107744E-16, 1.000000000000000000, 0.000000000000000000 ) ) ;
#3659=LINE ( 'NONE', #434, #1132 ) ;
#3664=CARTESIAN_POINT ( 'NONE',  ( 5.009003980371977336E-06, 8.320472128100606877E-07, 17.65096039353565160 ) ) ;
#3668=DIRECTION ( 'NONE',  ( 1.000000000000000000, -1.076498916035107744E-16, -0.000000000000000000 ) ) ;
#3669=LINE ( 'NONE', #2958, #1136 ) ;
#3670=CARTESIAN_POINT ( 'NONE',  ( -6.869994990996020512, 6.397500832047212427, 17.65096039353565160 ) ) ;
#3671=VERTEX_POINT ( 'NONE', #2373 ) ;
#3674=CARTESIAN_POINT ( 'NONE',  ( -13.60367840868947908, 4.371228564879502620, 38.02566532807935573 ) ) ;
#3676=CARTESIAN_POINT ( 'NONE',  ( 14.12123511036389090, -2.182294823265078509, 29.52615613029221109 ) ) ;
#3685=ORIENTED_EDGE ( 'NONE', *, *, #2329, .T. ) ;
#3692=VECTOR ( 'NONE', #3423, 1000.000000000000000 ) ;
#3695=VECTOR ( 'NONE', #3126, 1000.000000000000000 ) ;
#3697=ORIENTED_EDGE ( 'NONE', *, *, #3152, .T. ) ;
#3698=EDGE_LOOP ( 'NONE', ( #2158, #4237, #3441, #1223 ) ) ;
#3704=DIRECTION ( 'NONE',  ( 1.000000000000000000, 0.000000000000000000, 0.000000000000000000 ) ) ;
#3705=DIRECTION ( 'NONE',  ( 0.000000000000000000, -1.000000000000000000, 0.000000000000000000 ) ) ;
#3707=CARTESIAN_POINT ( 'NONE',  ( 6.870005009003977925, 6.397500832047211539, 17.65096039353565160 ) ) ;
#3711=DIRECTION ( 'NONE',  ( -1.076498916035107621E-16, 1.000000000000000000, -0.000000000000000000 ) ) ;
#3712=DIRECTION ( 'NONE',  ( 1.000000000000000000, 0.000000000000000000, 0.000000000000000000 ) ) ;
#3714=ORIENTED_EDGE ( 'NONE', *, *, #3319, .F. ) ;
#3720=CARTESIAN_POINT ( 'NONE',  ( -14.28749499099602005, 8.320472128100606877E-07, 39.51346039353565942 ) ) ;
#3721=PRODUCT_DEFINITION_FORMATION_WITH_SPECIFIED_SOURCE ( 'ANY', '', #2825, .NOT_KNOWN. ) ;
#3727=CARTESIAN_POINT ( 'NONE',  ( 12.37117714425454551, 7.147500832047209762, 32.36596039353565857 ) ) ;
#3729=DIRECTION ( 'NONE',  ( 1.000000000000000000, -8.673617379884035472E-17, 0.000000000000000000 ) ) ;
#3737=VERTEX_POINT ( 'NONE', #2127 ) ;
#3739=CARTESIAN_POINT ( 'NONE',  ( -14.03250750257131152, 2.692405860157741415, 34.72743248988972198 ) ) ;
#3745=VERTEX_POINT ( 'NONE', #3608 ) ;
#3748=CARTESIAN_POINT ( 'NONE',  ( 7.620005009003977037, 6.397500832047211539, 17.65096039353565160 ) ) ;
#3750=CARTESIAN_POINT ( 'NONE',  ( 7.620005009003978813, 8.320472119897684647E-07, 32.36596039353566567 ) ) ;
#3752=CARTESIAN_POINT ( 'NONE',  ( 0.000000000000000000, 0.000000000000000000, 0.000000000000000000 ) ) ;
#3762=ORIENTED_EDGE ( 'NONE', *, *, #520, .T. ) ;
#3763=DIRECTION ( 'NONE',  ( 0.000000000000000000, 1.000000000000000000, 0.000000000000000000 ) ) ;
#3766=CARTESIAN_POINT ( 'NONE',  ( 18.74250500900397753, 3.573750832047210224, 32.36596039353566567 ) ) ;
#3767=AXIS2_PLACEMENT_3D ( 'NONE', #3750, #4437, #1600 ) ;
#3771=ORIENTED_EDGE ( 'NONE', *, *, #1763, .T. ) ;
#3772=CARTESIAN_POINT ( 'NONE',  ( -14.26330390617519761, 0.9521795732501526777, 39.46544505580351370 ) ) ;
#3776=( NAMED_UNIT ( * ) SI_UNIT ( $, .STERADIAN. ) SOLID_ANGLE_UNIT ( ) );
#3777=CARTESIAN_POINT ( 'NONE',  ( -3.749994990996019961, 8.320472131353213394E-07, 17.65096039353565160 ) ) ;
#3778=CARTESIAN_POINT ( 'NONE',  ( 13.66282078896143659, 4.183338644556793717, 38.16598501014196643 ) ) ;
#3779=LINE ( 'NONE', #862, #7 ) ;
#3780=CARTESIAN_POINT ( 'NONE',  ( -7.619994990996017847, 12.08587093932537826, 39.51346039353565232 ) ) ;
#3784=VERTEX_POINT ( 'NONE', #2194 ) ;
#3786=CIRCLE ( 'NONE', #2278, 1.499999999999999556 ) ;
#3798=CARTESIAN_POINT ( 'NONE',  ( 14.26329420569817685, 0.9536349444224723193, 39.46541283322252980 ) ) ;
#3801=ADVANCED_FACE ( 'NONE', ( #1781 ), #3209, .T. ) ;
#3802=CARTESIAN_POINT ( 'NONE',  ( 13.83942688247485897, -3.550395471754214771, 32.83659103844913574 ) ) ;
#3808=VERTEX_POINT ( 'NONE', #4363 ) ;
#3809=AXIS2_PLACEMENT_3D ( 'NONE', #2355, #2625, #2312 ) ;
#3812=CYLINDRICAL_SURFACE ( 'NONE', #1118, 3.573749999999999538 ) ;
#3815=VECTOR ( 'NONE', #3621, 1000.000000000000000 ) ;
#3821=CARTESIAN_POINT ( 'NONE',  ( -14.28160183601729472, -0.4706309645614943360, 35.91635743244306411 ) ) ;
#3832=ORIENTED_EDGE ( 'NONE', *, *, #1769, .T. ) ;
#3835=EDGE_CURVE ( 'NONE', #3411, #4497, #922, .T. ) ;
#3837=DIRECTION ( 'NONE',  ( 0.000000000000000000, 0.000000000000000000, 1.000000000000000000 ) ) ;
#3842=AXIS2_PLACEMENT_3D ( 'NONE', #898, #4383, #4022 ) ;
#3843=CARTESIAN_POINT ( 'NONE',  ( -14.26328418769022122, -0.9536332803280443970, 39.46541283322252980 ) ) ;
#3844=CARTESIAN_POINT ( 'NONE',  ( 14.17128811577592451, -1.877060880510151852, 39.27869980365568381 ) ) ;
#3845=CARTESIAN_POINT ( 'NONE',  ( 13.83333314027810346, -3.573749167952787964, 32.60299647559080682 ) ) ;
#3848=CARTESIAN_POINT ( 'NONE',  ( -8.369994990996019624, -6.397499167952786614, 32.36596039353565857 ) ) ;
#3853=CARTESIAN_POINT ( 'NONE',  ( 18.74250500900397753, 8.320472107924325483E-07, 32.36596039353566567 ) ) ;
#3856=ORIENTED_EDGE ( 'NONE', *, *, #166, .F. ) ;
#3857=EDGE_CURVE ( 'NONE', #2299, #2304, #436, .T. ) ;
#3861=CYLINDRICAL_SURFACE ( 'NONE', #4043, 0.7500000000000006661 ) ;
#3862=CARTESIAN_POINT ( 'NONE',  ( -14.25898756740889439, -0.9310840564244263762, 35.82426841225251479 ) ) ;
#3863=CARTESIAN_POINT ( 'NONE',  ( 13.11669703816544619, -5.666583100918747284, 36.72824904517413103 ) ) ;
#3864=DIRECTION ( 'NONE',  ( -0.000000000000000000, -0.000000000000000000, -1.000000000000000000 ) ) ;
#3866=EDGE_CURVE ( 'NONE', #2091, #4049, #2675, .T. ) ;
#3870=AXIS2_PLACEMENT_3D ( 'NONE', #1543, #1522, #2935 ) ;
#3872=ORIENTED_EDGE ( 'NONE', *, *, #1934, .F. ) ;
#3874=ADVANCED_FACE ( 'NONE', ( #4006 ), #2217, .T. ) ;
#3878=CARTESIAN_POINT ( 'NONE',  ( 12.37117714425454551, -7.147499167952784838, 18.40096039353565160 ) ) ;
#3882=ORIENTED_EDGE ( 'NONE', *, *, #2192, .F. ) ;
#3884=CARTESIAN_POINT ( 'NONE',  ( 5.009003980371977336E-06, 8.320472128100606877E-07, 17.65096039353565160 ) ) ;
#3885=ORIENTED_EDGE ( 'NONE', *, *, #2190, .T. ) ;
#3889=CARTESIAN_POINT ( 'NONE',  ( -12.37116712624658810, -7.147499167952786614, 32.84697568125972822 ) ) ;
#3900=DIRECTION ( 'NONE',  ( 1.000000000000000000, -1.076498916035107621E-16, -0.000000000000000000 ) ) ;
#3903=VERTEX_POINT ( 'NONE', #2365 ) ;
#3906=EDGE_CURVE ( 'NONE', #3059, #1488, #2780, .T. ) ;
#3911=VECTOR ( 'NONE', #3282, 1000.000000000000000 ) ;
#3912=VECTOR ( 'NONE', #2765, 1000.000000000000000 ) ;
#3913=DIRECTION ( 'NONE',  ( -0.000000000000000000, -0.000000000000000000, -1.000000000000000000 ) ) ;
#3914=CARTESIAN_POINT ( 'NONE',  ( 14.26331392418316213, -0.9521779091557251995, 39.46544505580351370 ) ) ;
#3915=CIRCLE ( 'NONE', #1150, 1.499999999999999556 ) ;
#3917=CARTESIAN_POINT ( 'NONE',  ( -14.24246651021981336, 1.153954063360001614, 28.97559098912187991 ) ) ;
#3923=CARTESIAN_POINT ( 'NONE',  ( -7.619994990996019624, 8.320472136303528048E-07, 32.36596039353566567 ) ) ;
#3926=ORIENTED_EDGE ( 'NONE', *, *, #233, .T. ) ;
#3934=DIRECTION ( 'NONE',  ( -1.000000000000000000, 1.076498916035107744E-16, 0.000000000000000000 ) ) ;
#3936=EDGE_CURVE ( 'NONE', #3411, #1208, #162, .T. ) ;
#3937=EDGE_CURVE ( 'NONE', #3784, #195, #304, .T. ) ;
#3939=CARTESIAN_POINT ( 'NONE',  ( -14.28749499099602005, 8.320472128100571937E-07, 28.79221039353566880 ) ) ;
#3944=EDGE_CURVE ( 'NONE', #1617, #230, #2767, .T. ) ;
#3945=EDGE_CURVE ( 'NONE', #2464, #2260, #2453, .T. ) ;
#3946=VERTEX_POINT ( 'NONE', #1775 ) ;
#3947=CARTESIAN_POINT ( 'NONE',  ( 14.20052877066713037, 1.589184853276433662, 35.57557690958116581 ) ) ;
#3949=CARTESIAN_POINT ( 'NONE',  ( 18.74250500900397753, 8.320472107924325483E-07, 32.36596039353566567 ) ) ;
#3951=ORIENTED_EDGE ( 'NONE', *, *, #4005, .T. ) ;
#3952=VERTEX_POINT ( 'NONE', #3199 ) ;
#3956=B_SPLINE_CURVE_WITH_KNOTS ( 'NONE', 3,
 ( #731, #2916, #428, #779, #1872, #4506, #1219, #3036, #2988, #2614, #3400, #1593, #174, #4457, #497, #4481, #550, #1197 ),
 .UNSPECIFIED., .F., .F.,
 ( 4, 2, 2, 2, 2, 2, 2, 2, 4 ),
 ( 0.005610345619348811042, 0.006311274135232912939, 0.007012202651117014837, 0.007713131167001116735, 0.008414059682885218633, 0.009114988198769319663, 0.009815916714653420694, 0.01051684523053752346, 0.01121777374642162449 ),
 .UNSPECIFIED. ) ;
#3960=CARTESIAN_POINT ( 'NONE',  ( 8.370005009003978813, 7.147500832047211539, 18.40096039353565160 ) ) ;
#3963=CARTESIAN_POINT ( 'NONE',  ( -13.83332312227014427, 3.573750832047213777, 32.36596039353566567 ) ) ;
#3964=CARTESIAN_POINT ( 'NONE',  ( -14.28749499099602005, 8.320472128100606877E-07, 3.790960393535649064 ) ) ;
#3966=FACE_OUTER_BOUND ( 'NONE', #2913, .T. ) ;
#3969=CARTESIAN_POINT ( 'NONE',  ( 12.13299322807326064, -7.545448496333294841, 17.73224578507567628 ) ) ;
#3973=DIRECTION ( 'NONE',  ( 0.000000000000000000, 0.000000000000000000, 1.000000000000000000 ) ) ;
#3974=FACE_OUTER_BOUND ( 'NONE', #982, .T. ) ;
#3977=ORIENTED_EDGE ( 'NONE', *, *, #993, .T. ) ;
#3990=FACE_OUTER_BOUND ( 'NONE', #1314, .T. ) ;
#3995=ORIENTED_EDGE ( 'NONE', *, *, #3033, .F. ) ;
#3996=CARTESIAN_POINT ( 'NONE',  ( 14.28750500900398279, 8.320472145953950175E-07, 35.93971039353566965 ) ) ;
#3998=DIRECTION ( 'NONE',  ( -1.000000000000000000, 1.076498916035107744E-16, 0.000000000000000000 ) ) ;
#3999=EDGE_CURVE ( 'NONE', #3808, #3059, #258, .T. ) ;
#4001=ORIENTED_EDGE ( 'NONE', *, *, #4074, .F. ) ;
#4005=EDGE_CURVE ( 'NONE', #3671, #1779, #1186, .T. ) ;
#4006=FACE_OUTER_BOUND ( 'NONE', #937, .T. ) ;
#4008=DIRECTION ( 'NONE',  ( -1.000000000000000000, 1.076498916035107744E-16, -0.000000000000000000 ) ) ;
#4017=CARTESIAN_POINT ( 'NONE',  ( 13.83333314027810701, 3.573750832047210668, 32.36596039353566567 ) ) ;
#4020=DIRECTION ( 'NONE',  ( 0.000000000000000000, 0.000000000000000000, 1.000000000000000000 ) ) ;
#4022=DIRECTION ( 'NONE',  ( 0.000000000000000000, -1.000000000000000000, 0.000000000000000000 ) ) ;
#4023=EDGE_CURVE ( 'NONE', #195, #4203, #888, .T. ) ;
#4025=VECTOR ( 'NONE', #1505, 1000.000000000000000 ) ;
#4026=ORIENTED_EDGE ( 'NONE', *, *, #2098, .T. ) ;
#4028=CARTESIAN_POINT ( 'NONE',  ( -14.12134855583884629, 2.181372335837979737, 35.20634009499998029 ) ) ;
#4029=VECTOR ( 'NONE', #825, 1000.000000000000000 ) ;
#4031=ORIENTED_EDGE ( 'NONE', *, *, #3256, .F. ) ;
#4032=AXIS2_PLACEMENT_3D ( 'NONE', #4592, #239, #4189 ) ;
#4038=CARTESIAN_POINT ( 'NONE',  ( 12.37117714425454551, -7.147499167952784838, 18.40096039353565160 ) ) ;
#4039=AXIS2_PLACEMENT_3D ( 'NONE', #466, #4421, #838 ) ;
#4043=AXIS2_PLACEMENT_3D ( 'NONE', #999, #3427, #4129 ) ;
#4049=VERTEX_POINT ( 'NONE', #1539 ) ;
#4054=ADVANCED_FACE ( 'NONE', ( #2952 ), #2208, .F. ) ;
#4056=ORIENTED_EDGE ( 'NONE', *, *, #2080, .T. ) ;
#4057=CARTESIAN_POINT ( 'NONE',  ( 14.99250500900398109, 7.147500832047209762, 32.36596039353565857 ) ) ;
#4061=DIRECTION ( 'NONE',  ( 1.000000000000000000, -1.076498916035107621E-16, -0.000000000000000000 ) ) ;
#4062=ORIENTED_EDGE ( 'NONE', *, *, #600, .F. ) ;
#4064=( GEOMETRIC_REPRESENTATION_CONTEXT ( 3 ) GLOBAL_UNCERTAINTY_ASSIGNED_CONTEXT ( ( #2348 ) ) GLOBAL_UNIT_ASSIGNED_CONTEXT ( ( #740, #1838, #42 ) ) REPRESENTATION_CONTEXT ( 'NONE', 'WORKASPACE' ) );
#4068=DIRECTION ( 'NONE',  ( 1.000000000000000000, 0.000000000000000000, 0.000000000000000000 ) ) ;
#4074=EDGE_CURVE ( 'NONE', #2770, #3535, #1116, .T. ) ;
#4075=ORIENTED_EDGE ( 'NONE', *, *, #1792, .F. ) ;
#4078=LINE ( 'NONE', #4408, #645 ) ;
#4081=ORIENTED_EDGE ( 'NONE', *, *, #951, .T. ) ;
#4089=ADVANCED_FACE ( 'NONE', ( #3640, #2904 ), #4350, .T. ) ;
#4091=EDGE_CURVE ( 'NONE', #680, #4479, #767, .T. ) ;
#4092=CARTESIAN_POINT ( 'NONE',  ( 18.74250500900397753, 8.320472107924325483E-07, 32.36596039353566567 ) ) ;
#4096=FACE_OUTER_BOUND ( 'NONE', #2607, .T. ) ;
#4107=CARTESIAN_POINT ( 'NONE',  ( 13.42356276806338400, 4.895988140896816887, 37.57830303755702062 ) ) ;
#4112=LINE ( 'NONE', #512, #3217 ) ;
#4114=EDGE_CURVE ( 'NONE', #2014, #1947, #2377, .T. ) ;
#4115=CARTESIAN_POINT ( 'NONE',  ( 7.620005009003978813, 8.320472118282937035E-07, 32.36596039353565857 ) ) ;
#4117=CARTESIAN_POINT ( 'NONE',  ( -14.24230558378153511, 1.156047234311700977, 35.75566482172504834 ) ) ;
#4125=AXIS2_PLACEMENT_3D ( 'NONE', #2044, #1391, #2396 ) ;
#4127=EDGE_CURVE ( 'NONE', #4497, #1617, #2835, .T. ) ;
#4129=DIRECTION ( 'NONE',  ( 0.000000000000000000, -1.000000000000000000, 0.000000000000000000 ) ) ;
#4132=CARTESIAN_POINT ( 'NONE',  ( 12.39926910906711477, 7.099461186627058495, 33.31797499930307538 ) ) ;
#4136=AXIS2_PLACEMENT_3D ( 'NONE', #1466, #2547, #40 ) ;
#4137=CARTESIAN_POINT ( 'NONE',  ( 7.620005009003977037, 6.397500832047211539, 18.40096039353565160 ) ) ;
#4144=CIRCLE ( 'NONE', #2480, 0.7499999999999997780 ) ;
#4146=ORIENTED_EDGE ( 'NONE', *, *, #1174, .T. ) ;
#4147=ORIENTED_EDGE ( 'NONE', *, *, #1247, .T. ) ;
#4148=CARTESIAN_POINT ( 'NONE',  ( -13.93189556199112644, 3.198158771919405563, 38.77513429737268780 ) ) ;
#4149=ADVANCED_FACE ( 'NONE', ( #1606 ), #1210, .F. ) ;
#4157=CARTESIAN_POINT ( 'NONE',  ( 14.16479065912717772, 1.882519613464290087, 39.26516300994396147 ) ) ;
#4159=DIRECTION ( 'NONE',  ( -1.355782318074878530E-16, -1.000000000000000000, 0.000000000000000000 ) ) ;
#4161=ORIENTED_EDGE ( 'NONE', *, *, #2186, .F. ) ;
#4162=CARTESIAN_POINT ( 'NONE',  ( -11.90638613189174144, -7.897499167952782173, 17.65096039353565160 ) ) ;
#4171=ORIENTED_EDGE ( 'NONE', *, *, #3501, .F. ) ;
#4175=CARTESIAN_POINT ( 'NONE',  ( -12.87895030840308230, -6.192406806261855579, 35.96538579746959385 ) ) ;
#4176=CARTESIAN_POINT ( 'NONE',  ( 13.23919053713719407, -5.374173505363492254, 37.08379739163954980 ) ) ;
#4178=AXIS2_PLACEMENT_3D ( 'NONE', #2202, #1857, #2176 ) ;
#4179=CARTESIAN_POINT ( 'NONE',  ( 14.28168039487356289, -0.4681722336210599189, 35.91662862617997121 ) ) ;
#4183=AXIS2_PLACEMENT_3D ( 'NONE', #1585, #168, #2630 ) ;
#4189=DIRECTION ( 'NONE',  ( -1.076498916035107621E-16, 1.000000000000000000, 0.000000000000000000 ) ) ;
#4192=AXIS2_PLACEMENT_3D ( 'NONE', #3664, #439, #4304 ) ;
#4197=CARTESIAN_POINT ( 'NONE',  ( -13.83081082357190361, -3.605823043002055694, 38.55467339862568110 ) ) ;
#4198=FACE_OUTER_BOUND ( 'NONE', #4504, .T. ) ;
#4203=VERTEX_POINT ( 'NONE', #2720 ) ;
#4212=ORIENTED_EDGE ( 'NONE', *, *, #3999, .T. ) ;
#4213=TOROIDAL_SURFACE ( 'NONE', #4595, 1.500000000000000000, 0.7500000000000000000 ) ;
#4215=COLOUR_RGB ( '', 0.08235294, 0.09019608, 0.10196078) ;
#4217=ORIENTED_EDGE ( 'NONE', *, *, #4225, .T. ) ;
#4219=FACE_OUTER_BOUND ( 'NONE', #1315, .T. ) ;
#4225=EDGE_CURVE ( 'NONE', #3620, #2014, #4112, .T. ) ;
#4230=EDGE_CURVE ( 'NONE', #2126, #3252, #1579, .T. ) ;
#4231=ORIENTED_EDGE ( 'NONE', *, *, #2855, .T. ) ;
#4233=TOROIDAL_SURFACE ( 'NONE', #4311, 1.500000000000000000, 0.7500000000000000000 ) ;
#4236=ORIENTED_EDGE ( 'NONE', *, *, #265, .F. ) ;
#4237=ORIENTED_EDGE ( 'NONE', *, *, #2346, .F. ) ;
#4241=ORIENTED_EDGE ( 'NONE', *, *, #1582, .F. ) ;
#4247=B_SPLINE_CURVE_WITH_KNOTS ( 'NONE', 3,
 ( #625, #4609, #4179, #3123, #980, #1656, #2424, #962, #2379, #2067, #3502, #2356, #1394, #2402, #1999, #3802, #3845, #2809 ),
 .UNSPECIFIED., .F., .F.,
 ( 4, 2, 2, 2, 2, 2, 2, 2, 4 ),
 ( 0.01682620116816211167, 0.01752698813223788760, 0.01822777509631366005, 0.01892856206038943598, 0.01962934902446520843, 0.02033013598854098436, 0.02103092295261676029, 0.02173170991669253621, 0.02243249688076830867 ),
 .UNSPECIFIED. ) ;
#4251=CARTESIAN_POINT ( 'NONE',  ( -12.02319158376690567, -7.719183544751668791, 17.66665972527254880 ) ) ;
#4258=ADVANCED_FACE ( 'NONE', ( #3050 ), #160, .F. ) ;
#4261=ORIENTED_EDGE ( 'NONE', *, *, #900, .T. ) ;
#4263=VECTOR ( 'NONE', #988, 1000.000000000000000 ) ;
#4268=CARTESIAN_POINT ( 'NONE',  ( -14.24206966858596068, -1.158719165697675635, 35.75466352049880214 ) ) ;
#4269=CARTESIAN_POINT ( 'NONE',  ( 12.37117714425454551, -7.147499167952787502, 32.84705871297352076 ) ) ;
#4271=AXIS2_PLACEMENT_3D ( 'NONE', #1984, #1871, #3763 ) ;
#4284=LINE ( 'NONE', #704, #1360 ) ;
#4288=ORIENTED_EDGE ( 'NONE', *, *, #4091, .T. ) ;
#4293=CARTESIAN_POINT ( 'NONE',  ( -11.90638613189173789, 7.897500832047212427, 17.65096039353565160 ) ) ;
#4295=EDGE_CURVE ( 'NONE', #3952, #2867, #964, .T. ) ;
#4296=AXIS2_PLACEMENT_3D ( 'NONE', #409, #3913, #2872 ) ;
#4298=CARTESIAN_POINT ( 'NONE',  ( 8.370005009003978813, 7.147500832047211539, 18.40096039353565160 ) ) ;
#4301=DIRECTION ( 'NONE',  ( 1.000000000000000000, -1.076498916035107744E-16, -0.000000000000000000 ) ) ;
#4304=DIRECTION ( 'NONE',  ( 1.000000000000000000, 0.000000000000000000, -0.000000000000000000 ) ) ;
#4311=AXIS2_PLACEMENT_3D ( 'NONE', #841, #867, #2277 ) ;
#4313=EDGE_LOOP ( 'NONE', ( #904, #2961 ) ) ;
#4317=CARTESIAN_POINT ( 'NONE',  ( -3.749994990996019517, 3.750000832047212906, 18.79096039353565217 ) ) ;
#4319=DIRECTION ( 'NONE',  ( 0.000000000000000000, 0.000000000000000000, 1.000000000000000000 ) ) ;
#4322=DIRECTION ( 'NONE',  ( 1.000000000000000000, 0.000000000000000000, -0.000000000000000000 ) ) ;
#4324=SURFACE_STYLE_USAGE ( .BOTH. , #1882 ) ;
#4326=ORIENTED_EDGE ( 'NONE', *, *, #1276, .T. ) ;
#4327=CARTESIAN_POINT ( 'NONE',  ( 14.17575158735941088, 1.794122187399060930, 35.46543942424121809 ) ) ;
#4330=EDGE_CURVE ( 'NONE', #2464, #209, #3462, .T. ) ;
#4333=AXIS2_PLACEMENT_3D ( 'NONE', #1610, #2280, #4068 ) ;
#4337=ORIENTED_EDGE ( 'NONE', *, *, #4330, .F. ) ;
#4341=CARTESIAN_POINT ( 'NONE',  ( -13.83947321077509329, 3.550175980372930251, 31.89403414396633352 ) ) ;
#4342=DIRECTION ( 'NONE',  ( -0.000000000000000000, -0.000000000000000000, -1.000000000000000000 ) ) ;
#4343=AXIS2_PLACEMENT_3D ( 'NONE', #3923, #2117, #331 ) ;
#4346=CARTESIAN_POINT ( 'NONE',  ( -6.869994990996018736, 12.08587093932537826, 18.40096039353565160 ) ) ;
#4350=PLANE ( 'NONE',  #4192 ) ;
#4358=ORIENTED_EDGE ( 'NONE', *, *, #2450, .T. ) ;
#4361=VERTEX_POINT ( 'NONE', #4560 ) ;
#4363=CARTESIAN_POINT ( 'NONE',  ( -14.28749499099602005, 8.320472128100606877E-07, 39.51346039353565942 ) ) ;
#4366=VECTOR ( 'NONE', #1791, 1000.000000000000000 ) ;
#4367=VECTOR ( 'NONE', #2717, 1000.000000000000000 ) ;
#4368=CARTESIAN_POINT ( 'NONE',  ( -13.86261522604896257, -3.458704258809938370, 31.43673240174894801 ) ) ;
#4369=AXIS2_PLACEMENT_3D ( 'NONE', #652, #1722, #3506 ) ;
#4370=FACE_OUTER_BOUND ( 'NONE', #1427, .T. ) ;
#4383=DIRECTION ( 'NONE',  ( 1.000000000000000000, -1.076498916035107621E-16, -0.000000000000000000 ) ) ;
#4385=VERTEX_POINT ( 'NONE', #3526 ) ;
#4387=CARTESIAN_POINT ( 'NONE',  ( -14.20057228749327827, 1.588540649541856808, 35.57580161124558060 ) ) ;
#4392=CARTESIAN_POINT ( 'NONE',  ( -12.37116712624657033, 7.147500832047212427, 32.36596039353565857 ) ) ;
#4396=CARTESIAN_POINT ( 'NONE',  ( 12.02324309811277203, -7.719128299133020121, 17.66658805193229753 ) ) ;
#4398=CARTESIAN_POINT ( 'NONE',  ( 13.85858657070305711, 3.479382377821004013, 33.30553846872138024 ) ) ;
#4400=CYLINDRICAL_SURFACE ( 'NONE', #3109, 7.147499999999999076 ) ;
#4405=LINE ( 'NONE', #872, #915 ) ;
#4408=CARTESIAN_POINT ( 'NONE',  ( -7.619994990996017847, 6.397500832047212427, 32.36596039353565857 ) ) ;
#4417=CARTESIAN_POINT ( 'NONE',  ( -12.35745565209315444, 7.171352271666981970, 18.18649461234914710 ) ) ;
#4420=ORIENTED_EDGE ( 'NONE', *, *, #13, .F. ) ;
#4421=DIRECTION ( 'NONE',  ( 1.000000000000000000, 0.000000000000000000, 0.000000000000000000 ) ) ;
#4430=ORIENTED_EDGE ( 'NONE', *, *, #1836, .F. ) ;
#4434=LINE ( 'NONE', #525, #2371 ) ;
#4436=ORIENTED_EDGE ( 'NONE', *, *, #2510, .F. ) ;
#4437=DIRECTION ( 'NONE',  ( -1.000000000000000000, -1.076498916035107621E-16, 0.000000000000000000 ) ) ;
#4442=DIRECTION ( 'NONE',  ( -1.000000000000000000, 1.076498916035107621E-16, 0.000000000000000000 ) ) ;
#4444=EDGE_LOOP ( 'NONE', ( #1328, #3557, #287, #315 ) ) ;
#4457=CARTESIAN_POINT ( 'NONE',  ( 13.87971526468629690, 3.390392411081628143, 31.21208060327063194 ) ) ;
#4463=FACE_OUTER_BOUND ( 'NONE', #2729, .T. ) ;
#4464=CARTESIAN_POINT ( 'NONE',  ( 12.76962709079479019, 6.411762314134477947, 35.55869424641613818 ) ) ;
#4466=FACE_OUTER_BOUND ( 'NONE', #1867, .T. ) ;
#4473=CARTESIAN_POINT ( 'NONE',  ( -8.369994990996019624, -7.897499167952782173, 18.40096039353565160 ) ) ;
#4475=CARTESIAN_POINT ( 'NONE',  ( -7.619994990996017847, 6.397500832047212427, 32.36596039353565857 ) ) ;
#4476=EDGE_CURVE ( 'NONE', #1212, #3252, #1847, .T. ) ;
#4478=ORIENTED_EDGE ( 'NONE', *, *, #1763, .F. ) ;
#4479=VERTEX_POINT ( 'NONE', #1104 ) ;
#4481=CARTESIAN_POINT ( 'NONE',  ( 13.83943987092327177, 3.550346313559760603, 31.89501272945897270 ) ) ;
#4483=AXIS2_PLACEMENT_3D ( 'NONE', #3752, #129, #3704 ) ;
#4488=AXIS2_PLACEMENT_3D ( 'NONE', #2846, #1045, #2100 ) ;
#4489=CARTESIAN_POINT ( 'NONE',  ( -8.369994990996019624, -7.147499167952784838, 32.36596039353565857 ) ) ;
#4497=VERTEX_POINT ( 'NONE', #2152 ) ;
#4502=VECTOR ( 'NONE', #2939, 1000.000000000000000 ) ;
#4503=DIRECTION ( 'NONE',  ( -0.000000000000000000, -0.000000000000000000, -1.000000000000000000 ) ) ;
#4504=EDGE_LOOP ( 'NONE', ( #2232, #774, #1235, #4161 ) ) ;
#4506=CARTESIAN_POINT ( 'NONE',  ( 14.20066698090924540, 1.587871178531814698, 29.15574023557984162 ) ) ;
#4509=EDGE_LOOP ( 'NONE', ( #4358, #373, #4430, #3113 ) ) ;
#4510=CARTESIAN_POINT ( 'NONE',  ( -7.619994990996019624, 3.573750832047213333, 32.36596039353566567 ) ) ;
#4512=DIRECTION ( 'NONE',  ( -1.000000000000000000, 8.673617379884035472E-17, 0.000000000000000000 ) ) ;
#4513=CARTESIAN_POINT ( 'NONE',  ( 14.05881085617579629, 2.555481233519228734, 39.04506677964693750 ) ) ;
#4514=CARTESIAN_POINT ( 'NONE',  ( -8.369994990996016071, 7.147500832047212427, 17.65096039353565160 ) ) ;
#4519=DIRECTION ( 'NONE',  ( 0.000000000000000000, 0.000000000000000000, 1.000000000000000000 ) ) ;
#4522=CARTESIAN_POINT ( 'NONE',  ( 8.370005009003978813, 7.147500832047211539, 32.36596039353565857 ) ) ;
#4526=EDGE_LOOP ( 'NONE', ( #3576, #1693, #3856, #581 ) ) ;
#4527=VERTEX_POINT ( 'NONE', #3964 ) ;
#4533=CARTESIAN_POINT ( 'NONE',  ( -14.03259314636827781, -2.691943933906732589, 34.72792442121545520 ) ) ;
#4534=CARTESIAN_POINT ( 'NONE',  ( 13.83333314027809990, -3.573749167952787520, 32.12875308005140340 ) ) ;
#4535=DIRECTION ( 'NONE',  ( 1.000000000000000000, 0.000000000000000000, 0.000000000000000000 ) ) ;
#4536=CARTESIAN_POINT ( 'NONE',  ( -14.28749499099602183, -0.4675531348298848089, 28.79221039353566880 ) ) ;
#4541=CARTESIAN_POINT ( 'NONE',  ( -12.58715052442827442, 6.760359879724757270, 34.69836126359586359 ) ) ;
#4546=ADVANCED_FACE ( 'NONE', ( #4370 ), #2921, .T. ) ;
#4551=DIRECTION ( 'NONE',  ( 1.000000000000000000, 0.000000000000000000, 0.000000000000000000 ) ) ;
#4554=CARTESIAN_POINT ( 'NONE',  ( 7.620005009003977037, 12.08587093932537826, 39.51346039353565232 ) ) ;
#4560=CARTESIAN_POINT ( 'NONE',  ( 8.370005009003978813, -7.897499167952785726, 17.65096039353565160 ) ) ;
#4569=ORIENTED_EDGE ( 'NONE', *, *, #2269, .T. ) ;
#4573=EDGE_CURVE ( 'NONE', #919, #2304, #2146, .T. ) ;
#4574=ADVANCED_FACE ( 'NONE', ( #3990 ), #1158, .T. ) ;
#4576=DIRECTION ( 'NONE',  ( 0.000000000000000000, 0.000000000000000000, 1.000000000000000000 ) ) ;
#4578=EDGE_CURVE ( 'NONE', #2506, #230, #1437, .T. ) ;
#4579=CARTESIAN_POINT ( 'NONE',  ( -13.11702475164146264, -5.665798330090755286, 36.72925822850184829 ) ) ;
#4580=CARTESIAN_POINT ( 'NONE',  ( 13.93190557999908918, -3.198157107824978418, 38.77513429737269490 ) ) ;
#4587=LINE ( 'NONE', #545, #753 ) ;
#4590=CARTESIAN_POINT ( 'NONE',  ( -13.83927490936194360, 3.550949608386229528, 32.83276965945781711 ) ) ;
#4592=CARTESIAN_POINT ( 'NONE',  ( 8.370005009003978813, 8.320472119090310841E-07, 32.36596039353565857 ) ) ;
#4595=AXIS2_PLACEMENT_3D ( 'NONE', #2040, #2333, #4551 ) ;
#4599=ORIENTED_EDGE ( 'NONE', *, *, #1799, .F. ) ;
#4602=CARTESIAN_POINT ( 'NONE',  ( -8.369994990996019624, 8.320472137110901854E-07, 32.36596039353565857 ) ) ;
#4609=CARTESIAN_POINT ( 'NONE',  ( 14.28750500900398102, -0.2356504121955460829, 35.93971039353566965 ) ) ;
#4615=CIRCLE ( 'NONE', #2949, 14.28750000000000142 ) ;
#4625=CARTESIAN_POINT ( 'NONE',  ( -12.76961707278682923, -6.411760650040047693, 35.55869424641612397 ) ) ;
#4626=ADVANCED_FACE ( 'NONE', ( #3236 ), #12, .F. ) ;
#4627=CARTESIAN_POINT ( 'NONE',  ( -7.619994990996021400, -6.397499167952784838, 18.40096039353565160 ) ) ;
#4629=ORIENTED_EDGE ( 'NONE', *, *, #600, .T. ) ;
#4635=EDGE_CURVE ( 'NONE', #2793, #2774, #1187, .T. ) ;
ENDSEC;
END-ISO-10303-21;
